ISO-10303-21;
HEADER;
/* Generated by software containing ST-Developer
 * from STEP Tools, Inc. (www.steptools.com) 
 */

FILE_DESCRIPTION(
/* description */ (''),
/* implementation_level */ '2;1');

FILE_NAME(
/* name */ 
'01_Slotted_Foot_Base_with_Post_Socket_80x60.step',
/* time_stamp */ '2026-10-20T10:06:23-07:00',
/* author */ (''),
/* organization */ (''),
/* preprocessor_version */ 'ST-DEVELOPER v20.2',
/* originating_system */ 'Autodesk Translation Framework v15.15.0.0',
/* authorisation */ '');

FILE_SCHEMA (('AUTOMOTIVE_DESIGN { 1 0 10303 214 3 1 1 }'));
ENDSEC;

DATA;
#10=MECHANICAL_DESIGN_GEOMETRIC_PRESENTATION_REPRESENTATION('',(#460),#38611);
#432=SHAPE_REPRESENTATION_RELATIONSHIP('SRR','None',#38668,#446);
#446=ADVANCED_BREP_SHAPE_REPRESENTATION('',(#474),#38597);
#460=STYLED_ITEM('',(#38857),#474);
#474=MANIFOLD_SOLID_BREP('Foot',#16234);
#488=TOROIDAL_SURFACE('',#16513,1.75,0.15);
#490=B_SPLINE_SURFACE_WITH_KNOTS('',3,3,((#22029,#22030,#22031,#22032,#22033,
#22034,#22035,#22036,#22037,#22038,#22039,#22040,#22041,#22042,#22043,#22044,
#22045,#22046,#22047,#22048,#22049,#22050),(#22051,#22052,#22053,#22054,
#22055,#22056,#22057,#22058,#22059,#22060,#22061,#22062,#22063,#22064,#22065,
#22066,#22067,#22068,#22069,#22070,#22071,#22072),(#22073,#22074,#22075,
#22076,#22077,#22078,#22079,#22080,#22081,#22082,#22083,#22084,#22085,#22086,
#22087,#22088,#22089,#22090,#22091,#22092,#22093,#22094),(#22095,#22096,
#22097,#22098,#22099,#22100,#22101,#22102,#22103,#22104,#22105,#22106,#22107,
#22108,#22109,#22110,#22111,#22112,#22113,#22114,#22115,#22116)),
 .UNSPECIFIED.,.F.,.T.,.F.,(4,4),(4,1,1,1,1,1,1,1,1,1,1,1,1,1,1,1,1,1,1,
4),(0.,1.),(0.,0.0885228467060966,0.177045693412193,0.221307116765241,0.26556854011829,
0.354091386824386,0.442614233530483,0.486875656883531,0.531137080236579,
0.619659926942676,0.708182773648772,0.752444197001821,0.796705620354869,
0.840967043707917,0.885228467060966,0.973751313767062,1.01801273712011,
1.06227416047316,1.15079700717926,1.23931985388535),.UNSPECIFIED.);
#491=B_SPLINE_SURFACE_WITH_KNOTS('',3,3,((#22409,#22410,#22411,#22412,#22413,
#22414,#22415,#22416,#22417,#22418,#22419,#22420,#22421,#22422,#22423,#22424,
#22425,#22426),(#22427,#22428,#22429,#22430,#22431,#22432,#22433,#22434,
#22435,#22436,#22437,#22438,#22439,#22440,#22441,#22442,#22443,#22444),
(#22445,#22446,#22447,#22448,#22449,#22450,#22451,#22452,#22453,#22454,
#22455,#22456,#22457,#22458,#22459,#22460,#22461,#22462),(#22463,#22464,
#22465,#22466,#22467,#22468,#22469,#22470,#22471,#22472,#22473,#22474,#22475,
#22476,#22477,#22478,#22479,#22480)),.UNSPECIFIED.,.F.,.T.,.F.,(4,4),(4,
1,1,1,1,1,1,1,1,1,1,1,1,1,1,4),(0.,1.),(0.,0.0883566653548034,0.176713330709607,
0.26506999606441,0.353426661419213,0.441783326774017,0.485961659451418,
0.53013999212882,0.706853322838427,0.751031655515829,0.79520998819323,0.883566653548034,
0.971923318902837,1.06027998425764,1.14863664961244,1.23699331496725),
 .UNSPECIFIED.);
#510=B_SPLINE_CURVE_WITH_KNOTS('',3,(#22007,#22008,#22009,#22010,#22011,
#22012,#22013,#22014,#22015,#22016,#22017,#22018,#22019,#22020,#22021,#22022,
#22023,#22024,#22025,#22026,#22027,#22028),.UNSPECIFIED.,.T.,.F.,(4,1,1,
1,1,1,1,1,1,1,1,1,1,1,1,1,1,1,1,4),(-1.23931985388535,-1.15079700717926,
-1.06227416047316,-1.01801273712011,-0.973751313767062,-0.885228467060966,
-0.840967043707917,-0.796705620354869,-0.752444197001821,-0.708182773648772,
-0.619659926942676,-0.531137080236579,-0.486875656883531,-0.442614233530483,
-0.354091386824386,-0.26556854011829,-0.221307116765241,-0.177045693412193,
-0.0885228467060966,0.),.UNSPECIFIED.);
#511=B_SPLINE_CURVE_WITH_KNOTS('',3,(#22120,#22121,#22122,#22123,#22124,
#22125,#22126,#22127),.UNSPECIFIED.,.F.,.F.,(4,1,1,1,1,4),(0.,0.0885228467060966,
0.177045693412193,0.221307116765241,0.26556854011829,0.309829963471338),
 .UNSPECIFIED.);
#512=B_SPLINE_CURVE_WITH_KNOTS('',3,(#22128,#22129,#22130,#22131,#22132,
#22133,#22134,#22135,#22136,#22137,#22138,#22139,#22140,#22141,#22142,#22143,
#22144,#22145),.UNSPECIFIED.,.F.,.F.,(4,1,1,1,1,1,1,1,1,1,1,1,1,1,1,4),
(0.309829963471338,0.354091386824386,0.442614233530483,0.486875656883531,
0.531137080236579,0.619659926942676,0.708182773648772,0.752444197001821,
0.796705620354869,0.840967043707917,0.885228467060966,0.973751313767062,
1.01801273712011,1.06227416047316,1.15079700717926,1.23931985388535),
 .UNSPECIFIED.);
#513=B_SPLINE_CURVE_WITH_KNOTS('',3,(#22150,#22151,#22152,#22153,#22154,
#22155,#22156),.UNSPECIFIED.,.F.,.F.,(4,1,1,1,4),(0.,0.0883566653548034,
0.176713330709607,0.26506999606441,0.309248328741812),.UNSPECIFIED.);
#514=B_SPLINE_CURVE_WITH_KNOTS('',3,(#22157,#22158,#22159,#22160,#22161,
#22162,#22163,#22164,#22165,#22166,#22167,#22168,#22169,#22170,#22171),
 .UNSPECIFIED.,.F.,.F.,(4,1,1,1,1,1,1,1,1,1,1,1,4),(0.309248328741812,0.353426661419213,
0.441783326774017,0.485961659451418,0.53013999212882,0.706853322838427,
0.751031655515829,0.79520998819323,0.883566653548034,0.971923318902837,
1.06027998425764,1.14863664961244,1.23699331496725),.UNSPECIFIED.);
#515=B_SPLINE_CURVE_WITH_KNOTS('',3,(#22483,#22484,#22485,#22486,#22487,
#22488,#22489,#22490,#22491,#22492,#22493,#22494,#22495,#22496,#22497,#22498,
#22499,#22500),.UNSPECIFIED.,.T.,.F.,(4,1,1,1,1,1,1,1,1,1,1,1,1,1,1,4),
(-1.23699331496725,-1.14863664961244,-1.06027998425764,-0.971923318902837,
-0.883566653548034,-0.79520998819323,-0.751031655515829,-0.706853322838427,
-0.53013999212882,-0.485961659451418,-0.441783326774017,-0.353426661419213,
-0.26506999606441,-0.176713330709607,-0.0883566653548034,0.),
 .UNSPECIFIED.);
#877=CYLINDRICAL_SURFACE('',#16433,1.);
#878=CYLINDRICAL_SURFACE('',#16435,0.205);
#879=CYLINDRICAL_SURFACE('',#16453,0.4);
#880=CYLINDRICAL_SURFACE('',#16456,0.4);
#881=CYLINDRICAL_SURFACE('',#16506,1.6);
#882=CYLINDRICAL_SURFACE('',#16551,0.325);
#883=CYLINDRICAL_SURFACE('',#16555,0.325);
#884=CYLINDRICAL_SURFACE('',#16573,0.4);
#885=CYLINDRICAL_SURFACE('',#16575,0.4);
#886=CYLINDRICAL_SURFACE('',#16577,0.325);
#887=CYLINDRICAL_SURFACE('',#16580,0.325);
#1159=FACE_BOUND('',#2713,.T.);
#1160=FACE_BOUND('',#2716,.T.);
#1161=FACE_BOUND('',#2766,.T.);
#1162=FACE_BOUND('',#2769,.T.);
#1205=CIRCLE('',#16425,1.0287867965644);
#1206=CIRCLE('',#16426,1.08);
#1207=CIRCLE('',#16428,1.0212132034356);
#1208=CIRCLE('',#16430,1.54);
#1209=CIRCLE('',#16432,1.);
#1210=CIRCLE('',#16434,1.);
#1211=CIRCLE('',#16445,0.378786796564403);
#1212=CIRCLE('',#16446,0.4);
#1213=CIRCLE('',#16449,0.378786796564403);
#1214=CIRCLE('',#16450,0.4);
#1215=CIRCLE('',#16454,0.4);
#1216=CIRCLE('',#16457,0.4);
#1217=CIRCLE('',#16461,0.361213203435596);
#1218=CIRCLE('',#16462,0.31);
#1219=CIRCLE('',#16465,0.361213203435596);
#1220=CIRCLE('',#16466,0.31);
#1221=CIRCLE('',#16475,0.363786796564403);
#1222=CIRCLE('',#16476,0.415);
#1223=CIRCLE('',#16481,0.363786796564403);
#1224=CIRCLE('',#16482,0.415);
#1225=CIRCLE('',#16486,0.361213203435596);
#1226=CIRCLE('',#16487,0.31);
#1227=CIRCLE('',#16490,0.361213203435596);
#1228=CIRCLE('',#16491,0.31);
#1229=CIRCLE('',#16495,0.363786796564403);
#1230=CIRCLE('',#16496,0.415);
#1231=CIRCLE('',#16501,0.363786796564403);
#1232=CIRCLE('',#16502,0.415);
#1233=CIRCLE('',#16505,1.75);
#1234=CIRCLE('',#16507,1.6);
#1235=CIRCLE('',#16508,1.6);
#1236=CIRCLE('',#16509,1.6);
#1237=CIRCLE('',#16511,1.5787867965644);
#1238=CIRCLE('',#16514,0.15);
#1239=CIRCLE('',#16519,0.4);
#1240=CIRCLE('',#16520,0.36);
#1241=CIRCLE('',#16523,0.4);
#1242=CIRCLE('',#16524,0.36);
#1243=CIRCLE('',#16528,0.365);
#1244=CIRCLE('',#16529,0.325);
#1245=CIRCLE('',#16533,0.365);
#1246=CIRCLE('',#16534,0.325);
#1247=CIRCLE('',#16538,0.365);
#1248=CIRCLE('',#16539,0.325);
#1249=CIRCLE('',#16543,0.365);
#1250=CIRCLE('',#16544,0.325);
#1251=CIRCLE('',#16547,0.36);
#1252=CIRCLE('',#16550,0.36);
#1253=CIRCLE('',#16552,0.325);
#1254=CIRCLE('',#16556,0.325);
#1255=CIRCLE('',#16560,0.4);
#1256=CIRCLE('',#16563,0.4);
#1257=CIRCLE('',#16568,0.325);
#1258=CIRCLE('',#16572,0.325);
#1672=CONICAL_SURFACE('',#16424,1.0543933982822,1.17809724509618);
#1673=CONICAL_SURFACE('',#16427,1.025,0.785398163397448);
#1674=CONICAL_SURFACE('',#16431,1.0106066017178,0.392699081698721);
#1675=CONICAL_SURFACE('',#16444,0.389393398282202,0.392699081698728);
#1676=CONICAL_SURFACE('',#16448,0.389393398282202,0.392699081698728);
#1677=CONICAL_SURFACE('',#16460,0.335606601717798,1.17809724509618);
#1678=CONICAL_SURFACE('',#16464,0.335606601717798,1.17809724509618);
#1679=CONICAL_SURFACE('',#16469,0.37,0.785398163397451);
#1680=CONICAL_SURFACE('',#16471,0.37,0.785398163397451);
#1681=CONICAL_SURFACE('',#16474,0.389393398282202,1.17809724509617);
#1682=CONICAL_SURFACE('',#16480,0.389393398282202,1.17809724509617);
#1683=CONICAL_SURFACE('',#16485,0.335606601717798,1.17809724509618);
#1684=CONICAL_SURFACE('',#16489,0.335606601717798,1.17809724509618);
#1685=CONICAL_SURFACE('',#16494,0.389393398282202,1.17809724509617);
#1686=CONICAL_SURFACE('',#16500,0.389393398282202,1.17809724509617);
#1687=CONICAL_SURFACE('',#16510,1.5893933982822,0.392699081698725);
#1688=CONICAL_SURFACE('',#16512,1.57,0.785398163397448);
#1689=CONICAL_SURFACE('',#16518,0.38,0.785398163397451);
#1690=CONICAL_SURFACE('',#16522,0.38,0.785398163397451);
#1691=CONICAL_SURFACE('',#16527,0.345,0.785398163397448);
#1692=CONICAL_SURFACE('',#16532,0.345,0.785398163397448);
#1693=CONICAL_SURFACE('',#16537,0.345,0.785398163397448);
#1694=CONICAL_SURFACE('',#16542,0.345,0.785398163397448);
#1695=CONICAL_SURFACE('',#16546,0.38,0.785398163397451);
#1696=CONICAL_SURFACE('',#16549,0.38,0.785398163397451);
#1697=CONICAL_SURFACE('',#16559,0.37,0.785398163397451);
#1698=CONICAL_SURFACE('',#16562,0.37,0.785398163397451);
#1699=CONICAL_SURFACE('',#16565,0.355,0.785398163397448);
#1700=CONICAL_SURFACE('',#16567,0.355,0.785398163397448);
#1701=CONICAL_SURFACE('',#16569,0.355,0.785398163397448);
#1702=CONICAL_SURFACE('',#16571,0.355,0.785398163397448);
#1774=FACE_OUTER_BOUND('',#2691,.T.);
#1775=FACE_OUTER_BOUND('',#2692,.T.);
#1776=FACE_OUTER_BOUND('',#2693,.T.);
#1777=FACE_OUTER_BOUND('',#2694,.T.);
#1778=FACE_OUTER_BOUND('',#2695,.T.);
#1779=FACE_OUTER_BOUND('',#2696,.T.);
#1780=FACE_OUTER_BOUND('',#2697,.T.);
#1781=FACE_OUTER_BOUND('',#2698,.T.);
#1782=FACE_OUTER_BOUND('',#2699,.T.);
#1783=FACE_OUTER_BOUND('',#2700,.T.);
#1784=FACE_OUTER_BOUND('',#2701,.T.);
#1785=FACE_OUTER_BOUND('',#2702,.T.);
#1786=FACE_OUTER_BOUND('',#2703,.T.);
#1787=FACE_OUTER_BOUND('',#2704,.T.);
#1788=FACE_OUTER_BOUND('',#2705,.T.);
#1789=FACE_OUTER_BOUND('',#2706,.T.);
#1790=FACE_OUTER_BOUND('',#2707,.T.);
#1791=FACE_OUTER_BOUND('',#2708,.T.);
#1792=FACE_OUTER_BOUND('',#2709,.T.);
#1793=FACE_OUTER_BOUND('',#2710,.T.);
#1794=FACE_OUTER_BOUND('',#2711,.T.);
#1795=FACE_OUTER_BOUND('',#2712,.T.);
#1796=FACE_OUTER_BOUND('',#2714,.T.);
#1797=FACE_OUTER_BOUND('',#2715,.T.);
#1798=FACE_OUTER_BOUND('',#2717,.T.);
#1799=FACE_OUTER_BOUND('',#2718,.T.);
#1800=FACE_OUTER_BOUND('',#2719,.T.);
#1801=FACE_OUTER_BOUND('',#2720,.T.);
#1802=FACE_OUTER_BOUND('',#2721,.T.);
#1803=FACE_OUTER_BOUND('',#2722,.T.);
#1804=FACE_OUTER_BOUND('',#2723,.T.);
#1805=FACE_OUTER_BOUND('',#2724,.T.);
#1806=FACE_OUTER_BOUND('',#2725,.T.);
#1807=FACE_OUTER_BOUND('',#2726,.T.);
#1808=FACE_OUTER_BOUND('',#2727,.T.);
#1809=FACE_OUTER_BOUND('',#2728,.T.);
#1810=FACE_OUTER_BOUND('',#2729,.T.);
#1811=FACE_OUTER_BOUND('',#2730,.T.);
#1812=FACE_OUTER_BOUND('',#2731,.T.);
#1813=FACE_OUTER_BOUND('',#2732,.T.);
#1814=FACE_OUTER_BOUND('',#2733,.T.);
#1815=FACE_OUTER_BOUND('',#2734,.T.);
#1816=FACE_OUTER_BOUND('',#2735,.T.);
#1817=FACE_OUTER_BOUND('',#2736,.T.);
#1818=FACE_OUTER_BOUND('',#2737,.T.);
#1819=FACE_OUTER_BOUND('',#2738,.T.);
#1820=FACE_OUTER_BOUND('',#2739,.T.);
#1821=FACE_OUTER_BOUND('',#2740,.T.);
#1822=FACE_OUTER_BOUND('',#2741,.T.);
#1823=FACE_OUTER_BOUND('',#2742,.T.);
#1824=FACE_OUTER_BOUND('',#2743,.T.);
#1825=FACE_OUTER_BOUND('',#2744,.T.);
#1826=FACE_OUTER_BOUND('',#2745,.T.);
#1827=FACE_OUTER_BOUND('',#2746,.T.);
#1828=FACE_OUTER_BOUND('',#2747,.T.);
#1829=FACE_OUTER_BOUND('',#2748,.T.);
#1830=FACE_OUTER_BOUND('',#2749,.T.);
#1831=FACE_OUTER_BOUND('',#2750,.T.);
#1832=FACE_OUTER_BOUND('',#2751,.T.);
#1833=FACE_OUTER_BOUND('',#2752,.T.);
#1834=FACE_OUTER_BOUND('',#2753,.T.);
#1835=FACE_OUTER_BOUND('',#2754,.T.);
#1836=FACE_OUTER_BOUND('',#2755,.T.);
#1837=FACE_OUTER_BOUND('',#2756,.T.);
#1838=FACE_OUTER_BOUND('',#2757,.T.);
#1839=FACE_OUTER_BOUND('',#2758,.T.);
#1840=FACE_OUTER_BOUND('',#2759,.T.);
#1841=FACE_OUTER_BOUND('',#2760,.T.);
#1842=FACE_OUTER_BOUND('',#2761,.T.);
#1843=FACE_OUTER_BOUND('',#2762,.T.);
#1844=FACE_OUTER_BOUND('',#2763,.T.);
#1845=FACE_OUTER_BOUND('',#2764,.T.);
#1846=FACE_OUTER_BOUND('',#2765,.T.);
#1847=FACE_OUTER_BOUND('',#2767,.T.);
#1848=FACE_OUTER_BOUND('',#2768,.T.);
#1849=FACE_OUTER_BOUND('',#2770,.T.);
#1850=FACE_OUTER_BOUND('',#2771,.T.);
#1851=FACE_OUTER_BOUND('',#2772,.T.);
#1852=FACE_OUTER_BOUND('',#2773,.T.);
#1853=FACE_OUTER_BOUND('',#2774,.T.);
#1854=FACE_OUTER_BOUND('',#2775,.T.);
#1855=FACE_OUTER_BOUND('',#2776,.T.);
#1856=FACE_OUTER_BOUND('',#2777,.T.);
#1857=FACE_OUTER_BOUND('',#2778,.T.);
#1858=FACE_OUTER_BOUND('',#2779,.T.);
#1859=FACE_OUTER_BOUND('',#2780,.T.);
#1860=FACE_OUTER_BOUND('',#2781,.T.);
#1861=FACE_OUTER_BOUND('',#2782,.T.);
#1862=FACE_OUTER_BOUND('',#2783,.T.);
#1863=FACE_OUTER_BOUND('',#2784,.T.);
#1864=FACE_OUTER_BOUND('',#2785,.T.);
#1865=FACE_OUTER_BOUND('',#2786,.T.);
#1866=FACE_OUTER_BOUND('',#2787,.T.);
#1867=FACE_OUTER_BOUND('',#2788,.T.);
#1868=FACE_OUTER_BOUND('',#2789,.T.);
#1869=FACE_OUTER_BOUND('',#2790,.T.);
#1870=FACE_OUTER_BOUND('',#2791,.T.);
#1871=FACE_OUTER_BOUND('',#2792,.T.);
#1872=FACE_OUTER_BOUND('',#2793,.T.);
#1873=FACE_OUTER_BOUND('',#2794,.T.);
#1874=FACE_OUTER_BOUND('',#2795,.T.);
#1875=FACE_OUTER_BOUND('',#2796,.T.);
#1876=FACE_OUTER_BOUND('',#2797,.T.);
#1877=FACE_OUTER_BOUND('',#2798,.T.);
#1878=FACE_OUTER_BOUND('',#2799,.T.);
#1879=FACE_OUTER_BOUND('',#2800,.T.);
#1880=FACE_OUTER_BOUND('',#2801,.T.);
#1881=FACE_OUTER_BOUND('',#2802,.T.);
#1882=FACE_OUTER_BOUND('',#2803,.T.);
#1883=FACE_OUTER_BOUND('',#2804,.T.);
#1884=FACE_OUTER_BOUND('',#2805,.T.);
#1885=FACE_OUTER_BOUND('',#2806,.T.);
#1886=FACE_OUTER_BOUND('',#2807,.T.);
#1887=FACE_OUTER_BOUND('',#2808,.T.);
#1888=FACE_OUTER_BOUND('',#2809,.T.);
#1889=FACE_OUTER_BOUND('',#2810,.T.);
#1890=FACE_OUTER_BOUND('',#2811,.T.);
#1891=FACE_OUTER_BOUND('',#2812,.T.);
#1892=FACE_OUTER_BOUND('',#2813,.T.);
#1893=FACE_OUTER_BOUND('',#2814,.T.);
#1894=FACE_OUTER_BOUND('',#2815,.T.);
#1895=FACE_OUTER_BOUND('',#2816,.T.);
#1896=FACE_OUTER_BOUND('',#2817,.T.);
#1897=FACE_OUTER_BOUND('',#2818,.T.);
#2691=EDGE_LOOP('',(#10019,#10020,#10021,#10022,#10023,#10024));
#2692=EDGE_LOOP('',(#10025,#10026,#10027,#10028,#10029));
#2693=EDGE_LOOP('',(#10030,#10031,#10032,#10033,#10034,#10035));
#2694=EDGE_LOOP('',(#10036,#10037,#10038,#10039));
#2695=EDGE_LOOP('',(#10040,#10041,#10042,#10043,#10044,#10045));
#2696=EDGE_LOOP('',(#10046,#10047,#10048,#10049,#10050));
#2697=EDGE_LOOP('',(#10051,#10052,#10053,#10054,#10055,#10056));
#2698=EDGE_LOOP('',(#10057,#10058,#10059,#10060));
#2699=EDGE_LOOP('',(#10061,#10062,#10063,#10064,#10065));
#2700=EDGE_LOOP('',(#10066,#10067,#10068,#10069,#10070));
#2701=EDGE_LOOP('',(#10071,#10072,#10073,#10074,#10075,#10076));
#2702=EDGE_LOOP('',(#10077,#10078,#10079,#10080,#10081));
#2703=EDGE_LOOP('',(#10082,#10083,#10084,#10085));
#2704=EDGE_LOOP('',(#10086,#10087,#10088,#10089,#10090));
#2705=EDGE_LOOP('',(#10091,#10092,#10093,#10094,#10095,#10096));
#2706=EDGE_LOOP('',(#10097,#10098,#10099,#10100,#10101,#10102));
#2707=EDGE_LOOP('',(#10103,#10104,#10105,#10106));
#2708=EDGE_LOOP('',(#10107,#10108,#10109,#10110,#10111,#10112));
#2709=EDGE_LOOP('',(#10113,#10114,#10115,#10116,#10117,#10118));
#2710=EDGE_LOOP('',(#10119,#10120,#10121,#10122));
#2711=EDGE_LOOP('',(#10123,#10124,#10125,#10126));
#2712=EDGE_LOOP('',(#10127));
#2713=EDGE_LOOP('',(#10128));
#2714=EDGE_LOOP('',(#10129,#10130,#10131,#10132));
#2715=EDGE_LOOP('',(#10133,#10134,#10135,#10136));
#2716=EDGE_LOOP('',(#10137));
#2717=EDGE_LOOP('',(#10138,#10139,#10140,#10141,#10142));
#2718=EDGE_LOOP('',(#10143,#10144,#10145,#10146,#10147,#10148));
#2719=EDGE_LOOP('',(#10149,#10150,#10151,#10152,#10153,#10154));
#2720=EDGE_LOOP('',(#10155,#10156,#10157,#10158));
#2721=EDGE_LOOP('',(#10159,#10160,#10161,#10162,#10163,#10164));
#2722=EDGE_LOOP('',(#10165,#10166,#10167,#10168,#10169));
#2723=EDGE_LOOP('',(#10170,#10171,#10172,#10173,#10174,#10175));
#2724=EDGE_LOOP('',(#10176,#10177,#10178,#10179,#10180));
#2725=EDGE_LOOP('',(#10181,#10182,#10183,#10184));
#2726=EDGE_LOOP('',(#10185,#10186,#10187,#10188,#10189));
#2727=EDGE_LOOP('',(#10190,#10191,#10192,#10193));
#2728=EDGE_LOOP('',(#10194,#10195,#10196,#10197));
#2729=EDGE_LOOP('',(#10198,#10199,#10200,#10201));
#2730=EDGE_LOOP('',(#10202,#10203,#10204,#10205,#10206,#10207));
#2731=EDGE_LOOP('',(#10208,#10209,#10210,#10211));
#2732=EDGE_LOOP('',(#10212,#10213,#10214,#10215));
#2733=EDGE_LOOP('',(#10216,#10217,#10218,#10219));
#2734=EDGE_LOOP('',(#10220,#10221,#10222,#10223));
#2735=EDGE_LOOP('',(#10224,#10225,#10226,#10227));
#2736=EDGE_LOOP('',(#10228,#10229,#10230,#10231));
#2737=EDGE_LOOP('',(#10232,#10233,#10234,#10235));
#2738=EDGE_LOOP('',(#10236,#10237,#10238,#10239));
#2739=EDGE_LOOP('',(#10240,#10241,#10242,#10243));
#2740=EDGE_LOOP('',(#10244,#10245,#10246,#10247));
#2741=EDGE_LOOP('',(#10248,#10249,#10250,#10251));
#2742=EDGE_LOOP('',(#10252,#10253,#10254,#10255));
#2743=EDGE_LOOP('',(#10256,#10257,#10258,#10259));
#2744=EDGE_LOOP('',(#10260,#10261,#10262,#10263));
#2745=EDGE_LOOP('',(#10264,#10265,#10266,#10267));
#2746=EDGE_LOOP('',(#10268,#10269,#10270,#10271));
#2747=EDGE_LOOP('',(#10272,#10273,#10274,#10275));
#2748=EDGE_LOOP('',(#10276,#10277,#10278,#10279));
#2749=EDGE_LOOP('',(#10280,#10281,#10282,#10283));
#2750=EDGE_LOOP('',(#10284,#10285,#10286,#10287));
#2751=EDGE_LOOP('',(#10288,#10289,#10290,#10291));
#2752=EDGE_LOOP('',(#10292,#10293,#10294,#10295));
#2753=EDGE_LOOP('',(#10296,#10297,#10298,#10299));
#2754=EDGE_LOOP('',(#10300,#10301,#10302,#10303));
#2755=EDGE_LOOP('',(#10304,#10305,#10306,#10307));
#2756=EDGE_LOOP('',(#10308,#10309,#10310,#10311));
#2757=EDGE_LOOP('',(#10312,#10313,#10314,#10315));
#2758=EDGE_LOOP('',(#10316,#10317,#10318,#10319));
#2759=EDGE_LOOP('',(#10320,#10321,#10322,#10323));
#2760=EDGE_LOOP('',(#10324,#10325,#10326,#10327));
#2761=EDGE_LOOP('',(#10328,#10329,#10330,#10331));
#2762=EDGE_LOOP('',(#10332,#10333,#10334,#10335));
#2763=EDGE_LOOP('',(#10336,#10337,#10338,#10339));
#2764=EDGE_LOOP('',(#10340,#10341,#10342,#10343));
#2765=EDGE_LOOP('',(#10344,#10345,#10346,#10347,#10348,#10349,#10350,#10351,
#10352,#10353,#10354,#10355,#10356,#10357,#10358,#10359,#10360,#10361,#10362,
#10363,#10364,#10365,#10366,#10367));
#2766=EDGE_LOOP('',(#10368));
#2767=EDGE_LOOP('',(#10369,#10370,#10371,#10372,#10373));
#2768=EDGE_LOOP('',(#10374,#10375,#10376,#10377,#10378));
#2769=EDGE_LOOP('',(#10379));
#2770=EDGE_LOOP('',(#10380,#10381,#10382,#10383));
#2771=EDGE_LOOP('',(#10384,#10385,#10386,#10387));
#2772=EDGE_LOOP('',(#10388,#10389,#10390,#10391,#10392));
#2773=EDGE_LOOP('',(#10393));
#2774=EDGE_LOOP('',(#10394,#10395,#10396,#10397,#10398));
#2775=EDGE_LOOP('',(#10399,#10400,#10401,#10402,#10403,#10404));
#2776=EDGE_LOOP('',(#10405,#10406,#10407,#10408));
#2777=EDGE_LOOP('',(#10409,#10410,#10411,#10412));
#2778=EDGE_LOOP('',(#10413,#10414,#10415,#10416));
#2779=EDGE_LOOP('',(#10417,#10418,#10419,#10420,#10421));
#2780=EDGE_LOOP('',(#10422,#10423,#10424,#10425,#10426));
#2781=EDGE_LOOP('',(#10427,#10428,#10429,#10430));
#2782=EDGE_LOOP('',(#10431,#10432,#10433,#10434,#10435));
#2783=EDGE_LOOP('',(#10436,#10437,#10438,#10439,#10440));
#2784=EDGE_LOOP('',(#10441,#10442,#10443,#10444));
#2785=EDGE_LOOP('',(#10445,#10446,#10447,#10448,#10449));
#2786=EDGE_LOOP('',(#10450,#10451,#10452,#10453,#10454));
#2787=EDGE_LOOP('',(#10455,#10456,#10457,#10458));
#2788=EDGE_LOOP('',(#10459,#10460,#10461,#10462,#10463));
#2789=EDGE_LOOP('',(#10464,#10465,#10466,#10467,#10468));
#2790=EDGE_LOOP('',(#10469,#10470,#10471,#10472));
#2791=EDGE_LOOP('',(#10473,#10474,#10475,#10476,#10477));
#2792=EDGE_LOOP('',(#10478,#10479,#10480,#10481));
#2793=EDGE_LOOP('',(#10482,#10483,#10484,#10485));
#2794=EDGE_LOOP('',(#10486,#10487,#10488,#10489));
#2795=EDGE_LOOP('',(#10490,#10491,#10492,#10493));
#2796=EDGE_LOOP('',(#10494,#10495,#10496,#10497));
#2797=EDGE_LOOP('',(#10498,#10499,#10500,#10501));
#2798=EDGE_LOOP('',(#10502,#10503,#10504,#10505));
#2799=EDGE_LOOP('',(#10506,#10507,#10508,#10509));
#2800=EDGE_LOOP('',(#10510,#10511,#10512,#10513,#10514,#10515,#10516,#10517,
#10518,#10519,#10520,#10521,#10522,#10523,#10524,#10525,#10526,#10527,#10528,
#10529,#10530,#10531,#10532,#10533));
#2801=EDGE_LOOP('',(#10534,#10535,#10536,#10537));
#2802=EDGE_LOOP('',(#10538,#10539,#10540,#10541));
#2803=EDGE_LOOP('',(#10542,#10543,#10544,#10545));
#2804=EDGE_LOOP('',(#10546,#10547,#10548,#10549,#10550));
#2805=EDGE_LOOP('',(#10551,#10552,#10553,#10554));
#2806=EDGE_LOOP('',(#10555,#10556,#10557,#10558,#10559));
#2807=EDGE_LOOP('',(#10560,#10561,#10562,#10563));
#2808=EDGE_LOOP('',(#10564,#10565,#10566,#10567));
#2809=EDGE_LOOP('',(#10568,#10569,#10570,#10571,#10572));
#2810=EDGE_LOOP('',(#10573,#10574,#10575,#10576));
#2811=EDGE_LOOP('',(#10577,#10578,#10579,#10580));
#2812=EDGE_LOOP('',(#10581,#10582,#10583,#10584));
#2813=EDGE_LOOP('',(#10585,#10586,#10587,#10588));
#2814=EDGE_LOOP('',(#10589,#10590,#10591,#10592));
#2815=EDGE_LOOP('',(#10593,#10594,#10595,#10596));
#2816=EDGE_LOOP('',(#10597,#10598,#10599,#10600));
#2817=EDGE_LOOP('',(#10601,#10602,#10603,#10604));
#2818=EDGE_LOOP('',(#10605,#10606,#10607,#10608));
#3654=LINE('',#21838,#4878);
#3655=LINE('',#21840,#4879);
#3656=LINE('',#21842,#4880);
#3657=LINE('',#21844,#4881);
#3658=LINE('',#21846,#4882);
#3659=LINE('',#21847,#4883);
#3660=LINE('',#21850,#4884);
#3661=LINE('',#21852,#4885);
#3662=LINE('',#21854,#4886);
#3663=LINE('',#21855,#4887);
#3664=LINE('',#21858,#4888);
#3665=LINE('',#21860,#4889);
#3666=LINE('',#21862,#4890);
#3667=LINE('',#21863,#4891);
#3668=LINE('',#21866,#4892);
#3669=LINE('',#21867,#4893);
#3670=LINE('',#21870,#4894);
#3671=LINE('',#21872,#4895);
#3672=LINE('',#21874,#4896);
#3673=LINE('',#21875,#4897);
#3674=LINE('',#21878,#4898);
#3675=LINE('',#21880,#4899);
#3676=LINE('',#21881,#4900);
#3677=LINE('',#21885,#4901);
#3678=LINE('',#21887,#4902);
#3679=LINE('',#21889,#4903);
#3680=LINE('',#21891,#4904);
#3681=LINE('',#21893,#4905);
#3682=LINE('',#21894,#4906);
#3683=LINE('',#21897,#4907);
#3684=LINE('',#21899,#4908);
#3685=LINE('',#21900,#4909);
#3686=LINE('',#21903,#4910);
#3687=LINE('',#21905,#4911);
#3688=LINE('',#21906,#4912);
#3689=LINE('',#21909,#4913);
#3690=LINE('',#21911,#4914);
#3691=LINE('',#21912,#4915);
#3692=LINE('',#21916,#4916);
#3693=LINE('',#21918,#4917);
#3694=LINE('',#21920,#4918);
#3695=LINE('',#21922,#4919);
#3696=LINE('',#21924,#4920);
#3697=LINE('',#21925,#4921);
#3698=LINE('',#21928,#4922);
#3699=LINE('',#21930,#4923);
#3700=LINE('',#21932,#4924);
#3701=LINE('',#21933,#4925);
#3702=LINE('',#21936,#4926);
#3703=LINE('',#21937,#4927);
#3704=LINE('',#21940,#4928);
#3705=LINE('',#21942,#4929);
#3706=LINE('',#21943,#4930);
#3707=LINE('',#21947,#4931);
#3708=LINE('',#21949,#4932);
#3709=LINE('',#21951,#4933);
#3710=LINE('',#21953,#4934);
#3711=LINE('',#21955,#4935);
#3712=LINE('',#21956,#4936);
#3713=LINE('',#21959,#4937);
#3714=LINE('',#21961,#4938);
#3715=LINE('',#21963,#4939);
#3716=LINE('',#21965,#4940);
#3717=LINE('',#21966,#4941);
#3718=LINE('',#21969,#4942);
#3719=LINE('',#21970,#4943);
#3720=LINE('',#21973,#4944);
#3721=LINE('',#21975,#4945);
#3722=LINE('',#21977,#4946);
#3723=LINE('',#21978,#4947);
#3724=LINE('',#21981,#4948);
#3725=LINE('',#21983,#4949);
#3726=LINE('',#21984,#4950);
#3727=LINE('',#21989,#4951);
#3728=LINE('',#21993,#4952);
#3729=LINE('',#22000,#4953);
#3730=LINE('',#22004,#4954);
#3731=LINE('',#22118,#4955);
#3732=LINE('',#22148,#4956);
#3733=LINE('',#22175,#4957);
#3734=LINE('',#22177,#4958);
#3735=LINE('',#22179,#4959);
#3736=LINE('',#22181,#4960);
#3737=LINE('',#22183,#4961);
#3738=LINE('',#22184,#4962);
#3739=LINE('',#22187,#4963);
#3740=LINE('',#22189,#4964);
#3741=LINE('',#22190,#4965);
#3742=LINE('',#22193,#4966);
#3743=LINE('',#22195,#4967);
#3744=LINE('',#22197,#4968);
#3745=LINE('',#22198,#4969);
#3746=LINE('',#22201,#4970);
#3747=LINE('',#22203,#4971);
#3748=LINE('',#22204,#4972);
#3749=LINE('',#22208,#4973);
#3750=LINE('',#22210,#4974);
#3751=LINE('',#22212,#4975);
#3752=LINE('',#22214,#4976);
#3753=LINE('',#22216,#4977);
#3754=LINE('',#22217,#4978);
#3755=LINE('',#22220,#4979);
#3756=LINE('',#22222,#4980);
#3757=LINE('',#22224,#4981);
#3758=LINE('',#22225,#4982);
#3759=LINE('',#22228,#4983);
#3760=LINE('',#22229,#4984);
#3761=LINE('',#22232,#4985);
#3762=LINE('',#22234,#4986);
#3763=LINE('',#22235,#4987);
#3764=LINE('',#22239,#4988);
#3765=LINE('',#22245,#4989);
#3766=LINE('',#22246,#4990);
#3767=LINE('',#22247,#4991);
#3768=LINE('',#22253,#4992);
#3769=LINE('',#22255,#4993);
#3770=LINE('',#22257,#4994);
#3771=LINE('',#22258,#4995);
#3772=LINE('',#22261,#4996);
#3773=LINE('',#22262,#4997);
#3774=LINE('',#22265,#4998);
#3775=LINE('',#22269,#4999);
#3776=LINE('',#22270,#5000);
#3777=LINE('',#22273,#5001);
#3778=LINE('',#22276,#5002);
#3779=LINE('',#22279,#5003);
#3780=LINE('',#22281,#5004);
#3781=LINE('',#22283,#5005);
#3782=LINE('',#22284,#5006);
#3783=LINE('',#22288,#5007);
#3784=LINE('',#22294,#5008);
#3785=LINE('',#22295,#5009);
#3786=LINE('',#22296,#5010);
#3787=LINE('',#22300,#5011);
#3788=LINE('',#22305,#5012);
#3789=LINE('',#22306,#5013);
#3790=LINE('',#22307,#5014);
#3791=LINE('',#22309,#5015);
#3792=LINE('',#22311,#5016);
#3793=LINE('',#22313,#5017);
#3794=LINE('',#22315,#5018);
#3795=LINE('',#22319,#5019);
#3796=LINE('',#22320,#5020);
#3797=LINE('',#22323,#5021);
#3798=LINE('',#22328,#5022);
#3799=LINE('',#22329,#5023);
#3800=LINE('',#22332,#5024);
#3801=LINE('',#22333,#5025);
#3802=LINE('',#22336,#5026);
#3803=LINE('',#22337,#5027);
#3804=LINE('',#22340,#5028);
#3805=LINE('',#22345,#5029);
#3806=LINE('',#22346,#5030);
#3807=LINE('',#22349,#5031);
#3808=LINE('',#22350,#5032);
#3809=LINE('',#22354,#5033);
#3810=LINE('',#22360,#5034);
#3811=LINE('',#22361,#5035);
#3812=LINE('',#22362,#5036);
#3813=LINE('',#22365,#5037);
#3814=LINE('',#22370,#5038);
#3815=LINE('',#22371,#5039);
#3816=LINE('',#22374,#5040);
#3817=LINE('',#22376,#5041);
#3818=LINE('',#22377,#5042);
#3819=LINE('',#22381,#5043);
#3820=LINE('',#22385,#5044);
#3821=LINE('',#22387,#5045);
#3822=LINE('',#22388,#5046);
#3823=LINE('',#22391,#5047);
#3824=LINE('',#22392,#5048);
#3825=LINE('',#22395,#5049);
#3826=LINE('',#22397,#5050);
#3827=LINE('',#22398,#5051);
#3828=LINE('',#22401,#5052);
#3829=LINE('',#22405,#5053);
#3830=LINE('',#22482,#5054);
#3831=LINE('',#22505,#5055);
#3832=LINE('',#22512,#5056);
#3833=LINE('',#22514,#5057);
#3834=LINE('',#22520,#5058);
#3835=LINE('',#22522,#5059);
#3836=LINE('',#22523,#5060);
#3837=LINE('',#22526,#5061);
#3838=LINE('',#22528,#5062);
#3839=LINE('',#22529,#5063);
#3840=LINE('',#22533,#5064);
#3841=LINE('',#22539,#5065);
#3842=LINE('',#22540,#5066);
#3843=LINE('',#22541,#5067);
#3844=LINE('',#22544,#5068);
#3845=LINE('',#22549,#5069);
#3846=LINE('',#22550,#5070);
#3847=LINE('',#22553,#5071);
#3848=LINE('',#22555,#5072);
#3849=LINE('',#22556,#5073);
#3850=LINE('',#22560,#5074);
#3851=LINE('',#22564,#5075);
#3852=LINE('',#22565,#5076);
#3853=LINE('',#22568,#5077);
#3854=LINE('',#22570,#5078);
#3855=LINE('',#22571,#5079);
#3856=LINE('',#22575,#5080);
#3857=LINE('',#22579,#5081);
#3858=LINE('',#22580,#5082);
#3859=LINE('',#22583,#5083);
#3860=LINE('',#22585,#5084);
#3861=LINE('',#22586,#5085);
#3862=LINE('',#22589,#5086);
#3863=LINE('',#22593,#5087);
#3864=LINE('',#22596,#5088);
#3865=LINE('',#22597,#5089);
#3866=LINE('',#22601,#5090);
#3867=LINE('',#22605,#5091);
#3868=LINE('',#22606,#5092);
#3869=LINE('',#22609,#5093);
#3870=LINE('',#22613,#5094);
#3871=LINE('',#22614,#5095);
#3872=LINE('',#22619,#5096);
#3873=LINE('',#22622,#5097);
#3874=LINE('',#22625,#5098);
#3875=LINE('',#22626,#5099);
#3876=LINE('',#22629,#5100);
#3877=LINE('',#22632,#5101);
#3878=LINE('',#22637,#5102);
#3879=LINE('',#22640,#5103);
#3880=LINE('',#22641,#5104);
#3881=LINE('',#22645,#5105);
#3882=LINE('',#22647,#5106);
#3883=LINE('',#22652,#5107);
#3884=LINE('',#22657,#5108);
#3885=LINE('',#22659,#5109);
#3886=LINE('',#22662,#5110);
#3887=LINE('',#22665,#5111);
#3888=LINE('',#22667,#5112);
#4878=VECTOR('',#17811,1.);
#4879=VECTOR('',#17812,1.);
#4880=VECTOR('',#17813,1.);
#4881=VECTOR('',#17814,1.);
#4882=VECTOR('',#17815,1.);
#4883=VECTOR('',#17816,1.);
#4884=VECTOR('',#17819,1.);
#4885=VECTOR('',#17820,1.);
#4886=VECTOR('',#17821,1.);
#4887=VECTOR('',#17822,1.);
#4888=VECTOR('',#17825,1.);
#4889=VECTOR('',#17826,1.);
#4890=VECTOR('',#17827,1.);
#4891=VECTOR('',#17828,1.);
#4892=VECTOR('',#17831,1.);
#4893=VECTOR('',#17832,1.);
#4894=VECTOR('',#17835,1.);
#4895=VECTOR('',#17836,1.);
#4896=VECTOR('',#17837,1.);
#4897=VECTOR('',#17838,1.);
#4898=VECTOR('',#17841,1.);
#4899=VECTOR('',#17842,1.);
#4900=VECTOR('',#17843,1.);
#4901=VECTOR('',#17846,1.);
#4902=VECTOR('',#17847,1.);
#4903=VECTOR('',#17848,1.);
#4904=VECTOR('',#17849,1.);
#4905=VECTOR('',#17850,1.);
#4906=VECTOR('',#17851,1.);
#4907=VECTOR('',#17854,1.);
#4908=VECTOR('',#17855,1.);
#4909=VECTOR('',#17856,1.);
#4910=VECTOR('',#17859,1.);
#4911=VECTOR('',#17860,1.);
#4912=VECTOR('',#17861,1.);
#4913=VECTOR('',#17864,1.);
#4914=VECTOR('',#17865,1.);
#4915=VECTOR('',#17866,1.);
#4916=VECTOR('',#17869,1.);
#4917=VECTOR('',#17870,1.);
#4918=VECTOR('',#17871,1.);
#4919=VECTOR('',#17872,1.);
#4920=VECTOR('',#17873,1.);
#4921=VECTOR('',#17874,1.);
#4922=VECTOR('',#17877,1.);
#4923=VECTOR('',#17878,1.);
#4924=VECTOR('',#17879,1.);
#4925=VECTOR('',#17880,1.);
#4926=VECTOR('',#17883,1.);
#4927=VECTOR('',#17884,1.);
#4928=VECTOR('',#17887,1.);
#4929=VECTOR('',#17888,1.);
#4930=VECTOR('',#17889,1.);
#4931=VECTOR('',#17892,1.);
#4932=VECTOR('',#17893,1.);
#4933=VECTOR('',#17894,1.);
#4934=VECTOR('',#17895,1.);
#4935=VECTOR('',#17896,1.);
#4936=VECTOR('',#17897,1.);
#4937=VECTOR('',#17900,1.);
#4938=VECTOR('',#17901,1.);
#4939=VECTOR('',#17902,1.);
#4940=VECTOR('',#17903,1.);
#4941=VECTOR('',#17904,1.);
#4942=VECTOR('',#17907,1.);
#4943=VECTOR('',#17908,1.);
#4944=VECTOR('',#17911,1.);
#4945=VECTOR('',#17912,1.);
#4946=VECTOR('',#17913,1.);
#4947=VECTOR('',#17914,1.);
#4948=VECTOR('',#17917,1.);
#4949=VECTOR('',#17918,1.);
#4950=VECTOR('',#17919,1.);
#4951=VECTOR('',#17924,1.0543933982822);
#4952=VECTOR('',#17929,1.025);
#4953=VECTOR('',#17938,1.0106066017178);
#4954=VECTOR('',#17943,1.);
#4955=VECTOR('',#17946,1.);
#4956=VECTOR('',#17949,0.205);
#4957=VECTOR('',#17952,1.);
#4958=VECTOR('',#17953,1.);
#4959=VECTOR('',#17954,1.);
#4960=VECTOR('',#17955,1.);
#4961=VECTOR('',#17956,1.);
#4962=VECTOR('',#17957,1.);
#4963=VECTOR('',#17960,1.);
#4964=VECTOR('',#17961,1.);
#4965=VECTOR('',#17962,1.);
#4966=VECTOR('',#17965,1.);
#4967=VECTOR('',#17966,1.);
#4968=VECTOR('',#17967,1.);
#4969=VECTOR('',#17968,1.);
#4970=VECTOR('',#17971,1.);
#4971=VECTOR('',#17972,1.);
#4972=VECTOR('',#17973,1.);
#4973=VECTOR('',#17976,1.);
#4974=VECTOR('',#17977,1.);
#4975=VECTOR('',#17978,1.);
#4976=VECTOR('',#17979,1.);
#4977=VECTOR('',#17980,1.);
#4978=VECTOR('',#17981,1.);
#4979=VECTOR('',#17984,1.);
#4980=VECTOR('',#17985,1.);
#4981=VECTOR('',#17986,1.);
#4982=VECTOR('',#17987,1.);
#4983=VECTOR('',#17990,1.);
#4984=VECTOR('',#17991,1.);
#4985=VECTOR('',#17994,1.);
#4986=VECTOR('',#17995,1.);
#4987=VECTOR('',#17996,1.);
#4988=VECTOR('',#17999,1.);
#4989=VECTOR('',#18006,1.);
#4990=VECTOR('',#18007,1.);
#4991=VECTOR('',#18008,1.);
#4992=VECTOR('',#18017,1.);
#4993=VECTOR('',#18018,1.);
#4994=VECTOR('',#18019,1.);
#4995=VECTOR('',#18020,1.);
#4996=VECTOR('',#18023,1.);
#4997=VECTOR('',#18024,1.);
#4998=VECTOR('',#18027,1.);
#4999=VECTOR('',#18032,1.);
#5000=VECTOR('',#18033,1.);
#5001=VECTOR('',#18036,1.);
#5002=VECTOR('',#18041,1.);
#5003=VECTOR('',#18044,1.);
#5004=VECTOR('',#18045,1.);
#5005=VECTOR('',#18046,1.);
#5006=VECTOR('',#18047,1.);
#5007=VECTOR('',#18050,1.);
#5008=VECTOR('',#18057,1.);
#5009=VECTOR('',#18058,1.);
#5010=VECTOR('',#18059,1.);
#5011=VECTOR('',#18062,1.);
#5012=VECTOR('',#18069,1.);
#5013=VECTOR('',#18070,1.);
#5014=VECTOR('',#18071,1.);
#5015=VECTOR('',#18074,1.);
#5016=VECTOR('',#18077,1.);
#5017=VECTOR('',#18080,1.);
#5018=VECTOR('',#18083,1.);
#5019=VECTOR('',#18088,1.);
#5020=VECTOR('',#18089,1.);
#5021=VECTOR('',#18092,1.);
#5022=VECTOR('',#18099,1.);
#5023=VECTOR('',#18100,1.);
#5024=VECTOR('',#18103,1.);
#5025=VECTOR('',#18104,1.);
#5026=VECTOR('',#18107,1.);
#5027=VECTOR('',#18108,1.);
#5028=VECTOR('',#18111,1.);
#5029=VECTOR('',#18118,1.);
#5030=VECTOR('',#18119,1.);
#5031=VECTOR('',#18122,1.);
#5032=VECTOR('',#18123,1.);
#5033=VECTOR('',#18126,1.);
#5034=VECTOR('',#18133,1.);
#5035=VECTOR('',#18134,1.);
#5036=VECTOR('',#18135,1.);
#5037=VECTOR('',#18138,1.);
#5038=VECTOR('',#18145,1.);
#5039=VECTOR('',#18146,1.);
#5040=VECTOR('',#18149,1.);
#5041=VECTOR('',#18150,1.);
#5042=VECTOR('',#18151,1.);
#5043=VECTOR('',#18154,1.);
#5044=VECTOR('',#18161,1.);
#5045=VECTOR('',#18162,1.);
#5046=VECTOR('',#18163,1.);
#5047=VECTOR('',#18166,1.);
#5048=VECTOR('',#18167,1.);
#5049=VECTOR('',#18170,1.);
#5050=VECTOR('',#18171,1.);
#5051=VECTOR('',#18172,1.);
#5052=VECTOR('',#18175,1.);
#5053=VECTOR('',#18182,1.);
#5054=VECTOR('',#18187,1.);
#5055=VECTOR('',#18192,1.6);
#5056=VECTOR('',#18201,1.5893933982822);
#5057=VECTOR('',#18204,1.57);
#5058=VECTOR('',#18213,1.);
#5059=VECTOR('',#18214,1.);
#5060=VECTOR('',#18215,1.);
#5061=VECTOR('',#18218,1.);
#5062=VECTOR('',#18219,1.);
#5063=VECTOR('',#18220,1.);
#5064=VECTOR('',#18223,1.);
#5065=VECTOR('',#18230,1.);
#5066=VECTOR('',#18231,1.);
#5067=VECTOR('',#18232,1.);
#5068=VECTOR('',#18235,1.);
#5069=VECTOR('',#18242,1.);
#5070=VECTOR('',#18243,1.);
#5071=VECTOR('',#18246,1.);
#5072=VECTOR('',#18247,1.);
#5073=VECTOR('',#18248,1.);
#5074=VECTOR('',#18251,1.);
#5075=VECTOR('',#18258,1.);
#5076=VECTOR('',#18259,1.);
#5077=VECTOR('',#18262,1.);
#5078=VECTOR('',#18263,1.);
#5079=VECTOR('',#18264,1.);
#5080=VECTOR('',#18267,1.);
#5081=VECTOR('',#18274,1.);
#5082=VECTOR('',#18275,1.);
#5083=VECTOR('',#18278,1.);
#5084=VECTOR('',#18279,1.);
#5085=VECTOR('',#18280,1.);
#5086=VECTOR('',#18283,1.);
#5087=VECTOR('',#18290,1.);
#5088=VECTOR('',#18293,1.);
#5089=VECTOR('',#18294,1.);
#5090=VECTOR('',#18297,1.);
#5091=VECTOR('',#18304,1.);
#5092=VECTOR('',#18305,1.);
#5093=VECTOR('',#18308,1.);
#5094=VECTOR('',#18313,1.);
#5095=VECTOR('',#18314,1.);
#5096=VECTOR('',#18321,1.);
#5097=VECTOR('',#18326,1.);
#5098=VECTOR('',#18329,1.);
#5099=VECTOR('',#18330,1.);
#5100=VECTOR('',#18333,1.);
#5101=VECTOR('',#18338,1.);
#5102=VECTOR('',#18345,1.);
#5103=VECTOR('',#18348,1.);
#5104=VECTOR('',#18349,1.);
#5105=VECTOR('',#18356,1.);
#5106=VECTOR('',#18359,1.);
#5107=VECTOR('',#18368,1.);
#5108=VECTOR('',#18377,1.);
#5109=VECTOR('',#18380,1.);
#5110=VECTOR('',#18385,1.);
#5111=VECTOR('',#18390,1.);
#5112=VECTOR('',#18393,1.);
#6102=VERTEX_POINT('',#21836);
#6103=VERTEX_POINT('',#21837);
#6104=VERTEX_POINT('',#21839);
#6105=VERTEX_POINT('',#21841);
#6106=VERTEX_POINT('',#21843);
#6107=VERTEX_POINT('',#21845);
#6108=VERTEX_POINT('',#21849);
#6109=VERTEX_POINT('',#21851);
#6110=VERTEX_POINT('',#21853);
#6111=VERTEX_POINT('',#21857);
#6112=VERTEX_POINT('',#21859);
#6113=VERTEX_POINT('',#21861);
#6114=VERTEX_POINT('',#21865);
#6115=VERTEX_POINT('',#21869);
#6116=VERTEX_POINT('',#21871);
#6117=VERTEX_POINT('',#21873);
#6118=VERTEX_POINT('',#21877);
#6119=VERTEX_POINT('',#21879);
#6120=VERTEX_POINT('',#21883);
#6121=VERTEX_POINT('',#21884);
#6122=VERTEX_POINT('',#21886);
#6123=VERTEX_POINT('',#21888);
#6124=VERTEX_POINT('',#21890);
#6125=VERTEX_POINT('',#21892);
#6126=VERTEX_POINT('',#21896);
#6127=VERTEX_POINT('',#21898);
#6128=VERTEX_POINT('',#21902);
#6129=VERTEX_POINT('',#21904);
#6130=VERTEX_POINT('',#21908);
#6131=VERTEX_POINT('',#21910);
#6132=VERTEX_POINT('',#21914);
#6133=VERTEX_POINT('',#21915);
#6134=VERTEX_POINT('',#21917);
#6135=VERTEX_POINT('',#21919);
#6136=VERTEX_POINT('',#21921);
#6137=VERTEX_POINT('',#21923);
#6138=VERTEX_POINT('',#21927);
#6139=VERTEX_POINT('',#21929);
#6140=VERTEX_POINT('',#21931);
#6141=VERTEX_POINT('',#21935);
#6142=VERTEX_POINT('',#21939);
#6143=VERTEX_POINT('',#21941);
#6144=VERTEX_POINT('',#21945);
#6145=VERTEX_POINT('',#21946);
#6146=VERTEX_POINT('',#21948);
#6147=VERTEX_POINT('',#21950);
#6148=VERTEX_POINT('',#21952);
#6149=VERTEX_POINT('',#21954);
#6150=VERTEX_POINT('',#21958);
#6151=VERTEX_POINT('',#21960);
#6152=VERTEX_POINT('',#21962);
#6153=VERTEX_POINT('',#21964);
#6154=VERTEX_POINT('',#21968);
#6155=VERTEX_POINT('',#21972);
#6156=VERTEX_POINT('',#21974);
#6157=VERTEX_POINT('',#21976);
#6158=VERTEX_POINT('',#21980);
#6159=VERTEX_POINT('',#21982);
#6160=VERTEX_POINT('',#21986);
#6161=VERTEX_POINT('',#21988);
#6162=VERTEX_POINT('',#21992);
#6163=VERTEX_POINT('',#21996);
#6164=VERTEX_POINT('',#21999);
#6165=VERTEX_POINT('',#22003);
#6166=VERTEX_POINT('',#22006);
#6167=VERTEX_POINT('',#22117);
#6168=VERTEX_POINT('',#22119);
#6169=VERTEX_POINT('',#22147);
#6170=VERTEX_POINT('',#22149);
#6171=VERTEX_POINT('',#22173);
#6172=VERTEX_POINT('',#22174);
#6173=VERTEX_POINT('',#22176);
#6174=VERTEX_POINT('',#22178);
#6175=VERTEX_POINT('',#22180);
#6176=VERTEX_POINT('',#22182);
#6177=VERTEX_POINT('',#22186);
#6178=VERTEX_POINT('',#22188);
#6179=VERTEX_POINT('',#22192);
#6180=VERTEX_POINT('',#22194);
#6181=VERTEX_POINT('',#22196);
#6182=VERTEX_POINT('',#22200);
#6183=VERTEX_POINT('',#22202);
#6184=VERTEX_POINT('',#22206);
#6185=VERTEX_POINT('',#22207);
#6186=VERTEX_POINT('',#22209);
#6187=VERTEX_POINT('',#22211);
#6188=VERTEX_POINT('',#22213);
#6189=VERTEX_POINT('',#22215);
#6190=VERTEX_POINT('',#22219);
#6191=VERTEX_POINT('',#22221);
#6192=VERTEX_POINT('',#22223);
#6193=VERTEX_POINT('',#22227);
#6194=VERTEX_POINT('',#22231);
#6195=VERTEX_POINT('',#22233);
#6196=VERTEX_POINT('',#22237);
#6197=VERTEX_POINT('',#22238);
#6198=VERTEX_POINT('',#22243);
#6199=VERTEX_POINT('',#22244);
#6200=VERTEX_POINT('',#22252);
#6201=VERTEX_POINT('',#22254);
#6202=VERTEX_POINT('',#22256);
#6203=VERTEX_POINT('',#22260);
#6204=VERTEX_POINT('',#22264);
#6205=VERTEX_POINT('',#22268);
#6206=VERTEX_POINT('',#22272);
#6207=VERTEX_POINT('',#22278);
#6208=VERTEX_POINT('',#22280);
#6209=VERTEX_POINT('',#22282);
#6210=VERTEX_POINT('',#22286);
#6211=VERTEX_POINT('',#22287);
#6212=VERTEX_POINT('',#22292);
#6213=VERTEX_POINT('',#22293);
#6214=VERTEX_POINT('',#22298);
#6215=VERTEX_POINT('',#22299);
#6216=VERTEX_POINT('',#22304);
#6217=VERTEX_POINT('',#22318);
#6218=VERTEX_POINT('',#22322);
#6219=VERTEX_POINT('',#22327);
#6220=VERTEX_POINT('',#22331);
#6221=VERTEX_POINT('',#22335);
#6222=VERTEX_POINT('',#22339);
#6223=VERTEX_POINT('',#22344);
#6224=VERTEX_POINT('',#22348);
#6225=VERTEX_POINT('',#22352);
#6226=VERTEX_POINT('',#22353);
#6227=VERTEX_POINT('',#22358);
#6228=VERTEX_POINT('',#22359);
#6229=VERTEX_POINT('',#22364);
#6230=VERTEX_POINT('',#22369);
#6231=VERTEX_POINT('',#22373);
#6232=VERTEX_POINT('',#22375);
#6233=VERTEX_POINT('',#22379);
#6234=VERTEX_POINT('',#22380);
#6235=VERTEX_POINT('',#22386);
#6236=VERTEX_POINT('',#22390);
#6237=VERTEX_POINT('',#22394);
#6238=VERTEX_POINT('',#22396);
#6239=VERTEX_POINT('',#22400);
#6240=VERTEX_POINT('',#22407);
#6241=VERTEX_POINT('',#22481);
#6242=VERTEX_POINT('',#22502);
#6243=VERTEX_POINT('',#22504);
#6244=VERTEX_POINT('',#22506);
#6245=VERTEX_POINT('',#22510);
#6246=VERTEX_POINT('',#22519);
#6247=VERTEX_POINT('',#22521);
#6248=VERTEX_POINT('',#22525);
#6249=VERTEX_POINT('',#22527);
#6250=VERTEX_POINT('',#22531);
#6251=VERTEX_POINT('',#22532);
#6252=VERTEX_POINT('',#22537);
#6253=VERTEX_POINT('',#22538);
#6254=VERTEX_POINT('',#22543);
#6255=VERTEX_POINT('',#22548);
#6256=VERTEX_POINT('',#22552);
#6257=VERTEX_POINT('',#22554);
#6258=VERTEX_POINT('',#22558);
#6259=VERTEX_POINT('',#22559);
#6260=VERTEX_POINT('',#22567);
#6261=VERTEX_POINT('',#22569);
#6262=VERTEX_POINT('',#22573);
#6263=VERTEX_POINT('',#22574);
#6264=VERTEX_POINT('',#22582);
#6265=VERTEX_POINT('',#22584);
#6266=VERTEX_POINT('',#22588);
#6267=VERTEX_POINT('',#22595);
#6268=VERTEX_POINT('',#22599);
#6269=VERTEX_POINT('',#22600);
#6270=VERTEX_POINT('',#22608);
#6271=VERTEX_POINT('',#22612);
#6272=VERTEX_POINT('',#22618);
#6273=VERTEX_POINT('',#22624);
#6274=VERTEX_POINT('',#22628);
#6275=VERTEX_POINT('',#22635);
#6276=VERTEX_POINT('',#22639);
#7625=EDGE_CURVE('',#6102,#6103,#3654,.T.);
#7626=EDGE_CURVE('',#6103,#6104,#3655,.T.);
#7627=EDGE_CURVE('',#6104,#6105,#3656,.T.);
#7628=EDGE_CURVE('',#6105,#6106,#3657,.T.);
#7629=EDGE_CURVE('',#6106,#6107,#3658,.T.);
#7630=EDGE_CURVE('',#6107,#6102,#3659,.T.);
#7631=EDGE_CURVE('',#6108,#6105,#3660,.T.);
#7632=EDGE_CURVE('',#6109,#6108,#3661,.T.);
#7633=EDGE_CURVE('',#6110,#6109,#3662,.T.);
#7634=EDGE_CURVE('',#6110,#6106,#3663,.T.);
#7635=EDGE_CURVE('',#6104,#6111,#3664,.T.);
#7636=EDGE_CURVE('',#6112,#6111,#3665,.T.);
#7637=EDGE_CURVE('',#6113,#6112,#3666,.T.);
#7638=EDGE_CURVE('',#6108,#6113,#3667,.T.);
#7639=EDGE_CURVE('',#6114,#6103,#3668,.T.);
#7640=EDGE_CURVE('',#6111,#6114,#3669,.T.);
#7641=EDGE_CURVE('',#6114,#6115,#3670,.T.);
#7642=EDGE_CURVE('',#6115,#6116,#3671,.T.);
#7643=EDGE_CURVE('',#6116,#6117,#3672,.T.);
#7644=EDGE_CURVE('',#6117,#6112,#3673,.T.);
#7645=EDGE_CURVE('',#6117,#6118,#3674,.T.);
#7646=EDGE_CURVE('',#6118,#6119,#3675,.T.);
#7647=EDGE_CURVE('',#6113,#6119,#3676,.T.);
#7648=EDGE_CURVE('',#6120,#6121,#3677,.T.);
#7649=EDGE_CURVE('',#6121,#6122,#3678,.T.);
#7650=EDGE_CURVE('',#6122,#6123,#3679,.T.);
#7651=EDGE_CURVE('',#6123,#6124,#3680,.T.);
#7652=EDGE_CURVE('',#6124,#6125,#3681,.T.);
#7653=EDGE_CURVE('',#6125,#6120,#3682,.T.);
#7654=EDGE_CURVE('',#6126,#6121,#3683,.T.);
#7655=EDGE_CURVE('',#6127,#6126,#3684,.T.);
#7656=EDGE_CURVE('',#6122,#6127,#3685,.T.);
#7657=EDGE_CURVE('',#6128,#6120,#3686,.T.);
#7658=EDGE_CURVE('',#6129,#6128,#3687,.T.);
#7659=EDGE_CURVE('',#6126,#6129,#3688,.T.);
#7660=EDGE_CURVE('',#6125,#6130,#3689,.T.);
#7661=EDGE_CURVE('',#6130,#6131,#3690,.T.);
#7662=EDGE_CURVE('',#6128,#6131,#3691,.T.);
#7663=EDGE_CURVE('',#6132,#6133,#3692,.T.);
#7664=EDGE_CURVE('',#6133,#6134,#3693,.T.);
#7665=EDGE_CURVE('',#6134,#6135,#3694,.T.);
#7666=EDGE_CURVE('',#6135,#6136,#3695,.T.);
#7667=EDGE_CURVE('',#6136,#6137,#3696,.T.);
#7668=EDGE_CURVE('',#6137,#6132,#3697,.T.);
#7669=EDGE_CURVE('',#6134,#6138,#3698,.T.);
#7670=EDGE_CURVE('',#6138,#6139,#3699,.T.);
#7671=EDGE_CURVE('',#6140,#6139,#3700,.T.);
#7672=EDGE_CURVE('',#6140,#6135,#3701,.T.);
#7673=EDGE_CURVE('',#6141,#6133,#3702,.T.);
#7674=EDGE_CURVE('',#6138,#6141,#3703,.T.);
#7675=EDGE_CURVE('',#6132,#6142,#3704,.T.);
#7676=EDGE_CURVE('',#6142,#6143,#3705,.T.);
#7677=EDGE_CURVE('',#6143,#6141,#3706,.T.);
#7678=EDGE_CURVE('',#6144,#6145,#3707,.T.);
#7679=EDGE_CURVE('',#6145,#6146,#3708,.T.);
#7680=EDGE_CURVE('',#6146,#6147,#3709,.T.);
#7681=EDGE_CURVE('',#6147,#6148,#3710,.T.);
#7682=EDGE_CURVE('',#6148,#6149,#3711,.T.);
#7683=EDGE_CURVE('',#6149,#6144,#3712,.T.);
#7684=EDGE_CURVE('',#6146,#6150,#3713,.T.);
#7685=EDGE_CURVE('',#6151,#6150,#3714,.T.);
#7686=EDGE_CURVE('',#6151,#6152,#3715,.T.);
#7687=EDGE_CURVE('',#6152,#6153,#3716,.T.);
#7688=EDGE_CURVE('',#6153,#6147,#3717,.T.);
#7689=EDGE_CURVE('',#6154,#6145,#3718,.T.);
#7690=EDGE_CURVE('',#6150,#6154,#3719,.T.);
#7691=EDGE_CURVE('',#6155,#6144,#3720,.T.);
#7692=EDGE_CURVE('',#6156,#6155,#3721,.T.);
#7693=EDGE_CURVE('',#6156,#6157,#3722,.T.);
#7694=EDGE_CURVE('',#6154,#6157,#3723,.T.);
#7695=EDGE_CURVE('',#6157,#6158,#3724,.T.);
#7696=EDGE_CURVE('',#6158,#6159,#3725,.T.);
#7697=EDGE_CURVE('',#6159,#6151,#3726,.T.);
#7698=EDGE_CURVE('',#6160,#6160,#1205,.T.);
#7699=EDGE_CURVE('',#6160,#6161,#3727,.T.);
#7700=EDGE_CURVE('',#6161,#6161,#1206,.T.);
#7701=EDGE_CURVE('',#6160,#6162,#3728,.T.);
#7702=EDGE_CURVE('',#6162,#6162,#1207,.T.);
#7703=EDGE_CURVE('',#6163,#6163,#1208,.T.);
#7704=EDGE_CURVE('',#6162,#6164,#3729,.T.);
#7705=EDGE_CURVE('',#6164,#6164,#1209,.T.);
#7706=EDGE_CURVE('',#6164,#6165,#3730,.T.);
#7707=EDGE_CURVE('',#6165,#6165,#1210,.T.);
#7708=EDGE_CURVE('',#6166,#6166,#510,.T.);
#7709=EDGE_CURVE('',#6166,#6167,#3731,.T.);
#7710=EDGE_CURVE('',#6167,#6168,#511,.T.);
#7711=EDGE_CURVE('',#6168,#6167,#512,.T.);
#7712=EDGE_CURVE('',#6168,#6169,#3732,.T.);
#7713=EDGE_CURVE('',#6170,#6169,#513,.T.);
#7714=EDGE_CURVE('',#6169,#6170,#514,.T.);
#7715=EDGE_CURVE('',#6171,#6172,#3733,.T.);
#7716=EDGE_CURVE('',#6172,#6173,#3734,.T.);
#7717=EDGE_CURVE('',#6173,#6174,#3735,.T.);
#7718=EDGE_CURVE('',#6174,#6175,#3736,.T.);
#7719=EDGE_CURVE('',#6175,#6176,#3737,.T.);
#7720=EDGE_CURVE('',#6176,#6171,#3738,.T.);
#7721=EDGE_CURVE('',#6177,#6175,#3739,.T.);
#7722=EDGE_CURVE('',#6177,#6178,#3740,.T.);
#7723=EDGE_CURVE('',#6176,#6178,#3741,.T.);
#7724=EDGE_CURVE('',#6179,#6174,#3742,.T.);
#7725=EDGE_CURVE('',#6180,#6179,#3743,.T.);
#7726=EDGE_CURVE('',#6181,#6180,#3744,.T.);
#7727=EDGE_CURVE('',#6177,#6181,#3745,.T.);
#7728=EDGE_CURVE('',#6173,#6182,#3746,.T.);
#7729=EDGE_CURVE('',#6182,#6183,#3747,.T.);
#7730=EDGE_CURVE('',#6183,#6179,#3748,.T.);
#7731=EDGE_CURVE('',#6184,#6185,#3749,.T.);
#7732=EDGE_CURVE('',#6185,#6186,#3750,.T.);
#7733=EDGE_CURVE('',#6186,#6187,#3751,.T.);
#7734=EDGE_CURVE('',#6187,#6188,#3752,.T.);
#7735=EDGE_CURVE('',#6188,#6189,#3753,.T.);
#7736=EDGE_CURVE('',#6189,#6184,#3754,.T.);
#7737=EDGE_CURVE('',#6186,#6190,#3755,.T.);
#7738=EDGE_CURVE('',#6191,#6190,#3756,.T.);
#7739=EDGE_CURVE('',#6191,#6192,#3757,.T.);
#7740=EDGE_CURVE('',#6192,#6187,#3758,.T.);
#7741=EDGE_CURVE('',#6193,#6185,#3759,.T.);
#7742=EDGE_CURVE('',#6190,#6193,#3760,.T.);
#7743=EDGE_CURVE('',#6184,#6194,#3761,.T.);
#7744=EDGE_CURVE('',#6194,#6195,#3762,.T.);
#7745=EDGE_CURVE('',#6193,#6195,#3763,.T.);
#7746=EDGE_CURVE('',#6196,#6197,#3764,.T.);
#7747=EDGE_CURVE('',#6197,#6183,#1211,.T.);
#7748=EDGE_CURVE('',#6182,#6196,#1212,.T.);
#7749=EDGE_CURVE('',#6198,#6199,#3765,.T.);
#7750=EDGE_CURVE('',#6199,#6197,#3766,.T.);
#7751=EDGE_CURVE('',#6196,#6198,#3767,.T.);
#7752=EDGE_CURVE('',#6195,#6199,#1213,.T.);
#7753=EDGE_CURVE('',#6198,#6193,#1214,.T.);
#7754=EDGE_CURVE('',#6189,#6200,#3768,.T.);
#7755=EDGE_CURVE('',#6200,#6201,#3769,.T.);
#7756=EDGE_CURVE('',#6202,#6201,#3770,.T.);
#7757=EDGE_CURVE('',#6202,#6194,#3771,.T.);
#7758=EDGE_CURVE('',#6203,#6188,#3772,.T.);
#7759=EDGE_CURVE('',#6200,#6203,#3773,.T.);
#7760=EDGE_CURVE('',#6198,#6204,#3774,.T.);
#7761=EDGE_CURVE('',#6190,#6204,#1215,.T.);
#7762=EDGE_CURVE('',#6205,#6196,#3775,.T.);
#7763=EDGE_CURVE('',#6204,#6205,#3776,.T.);
#7764=EDGE_CURVE('',#6182,#6206,#3777,.T.);
#7765=EDGE_CURVE('',#6205,#6206,#1216,.T.);
#7766=EDGE_CURVE('',#6206,#6172,#3778,.T.);
#7767=EDGE_CURVE('',#6202,#6207,#3779,.T.);
#7768=EDGE_CURVE('',#6207,#6208,#3780,.T.);
#7769=EDGE_CURVE('',#6208,#6209,#3781,.T.);
#7770=EDGE_CURVE('',#6209,#6202,#3782,.T.);
#7771=EDGE_CURVE('',#6210,#6211,#3783,.T.);
#7772=EDGE_CURVE('',#6211,#6209,#1217,.T.);
#7773=EDGE_CURVE('',#6208,#6210,#1218,.T.);
#7774=EDGE_CURVE('',#6212,#6213,#3784,.T.);
#7775=EDGE_CURVE('',#6213,#6211,#3785,.T.);
#7776=EDGE_CURVE('',#6210,#6212,#3786,.T.);
#7777=EDGE_CURVE('',#6214,#6215,#3787,.T.);
#7778=EDGE_CURVE('',#6215,#6213,#1219,.T.);
#7779=EDGE_CURVE('',#6212,#6214,#1220,.T.);
#7780=EDGE_CURVE('',#6216,#6180,#3788,.T.);
#7781=EDGE_CURVE('',#6180,#6215,#3789,.T.);
#7782=EDGE_CURVE('',#6214,#6216,#3790,.T.);
#7783=EDGE_CURVE('',#6195,#6209,#3791,.T.);
#7784=EDGE_CURVE('',#6199,#6211,#3792,.T.);
#7785=EDGE_CURVE('',#6197,#6213,#3793,.T.);
#7786=EDGE_CURVE('',#6183,#6215,#3794,.T.);
#7787=EDGE_CURVE('',#6216,#6217,#3795,.T.);
#7788=EDGE_CURVE('',#6217,#6181,#3796,.T.);
#7789=EDGE_CURVE('',#6218,#6119,#3797,.T.);
#7790=EDGE_CURVE('',#6119,#6181,#1221,.T.);
#7791=EDGE_CURVE('',#6217,#6218,#1222,.T.);
#7792=EDGE_CURVE('',#6218,#6219,#3798,.T.);
#7793=EDGE_CURVE('',#6219,#6113,#3799,.T.);
#7794=EDGE_CURVE('',#6219,#6220,#3800,.T.);
#7795=EDGE_CURVE('',#6220,#6108,#3801,.T.);
#7796=EDGE_CURVE('',#6220,#6221,#3802,.T.);
#7797=EDGE_CURVE('',#6221,#6109,#3803,.T.);
#7798=EDGE_CURVE('',#6222,#6131,#3804,.T.);
#7799=EDGE_CURVE('',#6131,#6109,#1223,.T.);
#7800=EDGE_CURVE('',#6221,#6222,#1224,.T.);
#7801=EDGE_CURVE('',#6222,#6223,#3805,.T.);
#7802=EDGE_CURVE('',#6223,#6128,#3806,.T.);
#7803=EDGE_CURVE('',#6223,#6224,#3807,.T.);
#7804=EDGE_CURVE('',#6224,#6129,#3808,.T.);
#7805=EDGE_CURVE('',#6225,#6226,#3809,.T.);
#7806=EDGE_CURVE('',#6226,#6129,#1225,.T.);
#7807=EDGE_CURVE('',#6224,#6225,#1226,.T.);
#7808=EDGE_CURVE('',#6227,#6228,#3810,.T.);
#7809=EDGE_CURVE('',#6228,#6226,#3811,.T.);
#7810=EDGE_CURVE('',#6225,#6227,#3812,.T.);
#7811=EDGE_CURVE('',#6229,#6139,#3813,.T.);
#7812=EDGE_CURVE('',#6139,#6228,#1227,.T.);
#7813=EDGE_CURVE('',#6227,#6229,#1228,.T.);
#7814=EDGE_CURVE('',#6229,#6230,#3814,.T.);
#7815=EDGE_CURVE('',#6230,#6140,#3815,.T.);
#7816=EDGE_CURVE('',#6230,#6231,#3816,.T.);
#7817=EDGE_CURVE('',#6231,#6232,#3817,.T.);
#7818=EDGE_CURVE('',#6232,#6140,#3818,.T.);
#7819=EDGE_CURVE('',#6233,#6234,#3819,.T.);
#7820=EDGE_CURVE('',#6234,#6232,#1229,.T.);
#7821=EDGE_CURVE('',#6231,#6233,#1230,.T.);
#7822=EDGE_CURVE('',#6155,#6234,#3820,.T.);
#7823=EDGE_CURVE('',#6233,#6235,#3821,.T.);
#7824=EDGE_CURVE('',#6235,#6155,#3822,.T.);
#7825=EDGE_CURVE('',#6235,#6236,#3823,.T.);
#7826=EDGE_CURVE('',#6236,#6156,#3824,.T.);
#7827=EDGE_CURVE('',#6236,#6237,#3825,.T.);
#7828=EDGE_CURVE('',#6237,#6238,#3826,.T.);
#7829=EDGE_CURVE('',#6238,#6156,#3827,.T.);
#7830=EDGE_CURVE('',#6239,#6201,#3828,.T.);
#7831=EDGE_CURVE('',#6201,#6238,#1231,.T.);
#7832=EDGE_CURVE('',#6237,#6239,#1232,.T.);
#7833=EDGE_CURVE('',#6239,#6207,#3829,.T.);
#7834=EDGE_CURVE('',#6240,#6240,#1233,.T.);
#7835=EDGE_CURVE('',#6241,#6170,#3830,.T.);
#7836=EDGE_CURVE('',#6241,#6241,#515,.T.);
#7837=EDGE_CURVE('',#6242,#6242,#1234,.T.);
#7838=EDGE_CURVE('',#6242,#6243,#3831,.T.);
#7839=EDGE_CURVE('',#6244,#6243,#1235,.T.);
#7840=EDGE_CURVE('',#6243,#6244,#1236,.T.);
#7841=EDGE_CURVE('',#6245,#6245,#1237,.T.);
#7842=EDGE_CURVE('',#6245,#6242,#3832,.T.);
#7843=EDGE_CURVE('',#6163,#6245,#3833,.T.);
#7844=EDGE_CURVE('',#6244,#6240,#1238,.T.);
#7845=EDGE_CURVE('',#6171,#6246,#3834,.T.);
#7846=EDGE_CURVE('',#6246,#6247,#3835,.T.);
#7847=EDGE_CURVE('',#6247,#6206,#3836,.T.);
#7848=EDGE_CURVE('',#6102,#6248,#3837,.T.);
#7849=EDGE_CURVE('',#6248,#6249,#3838,.T.);
#7850=EDGE_CURVE('',#6249,#6115,#3839,.T.);
#7851=EDGE_CURVE('',#6250,#6251,#3840,.T.);
#7852=EDGE_CURVE('',#6251,#6141,#1239,.T.);
#7853=EDGE_CURVE('',#6143,#6250,#1240,.T.);
#7854=EDGE_CURVE('',#6252,#6253,#3841,.T.);
#7855=EDGE_CURVE('',#6253,#6251,#3842,.T.);
#7856=EDGE_CURVE('',#6250,#6252,#3843,.T.);
#7857=EDGE_CURVE('',#6254,#6127,#3844,.T.);
#7858=EDGE_CURVE('',#6127,#6253,#1241,.T.);
#7859=EDGE_CURVE('',#6252,#6254,#1242,.T.);
#7860=EDGE_CURVE('',#6254,#6255,#3845,.T.);
#7861=EDGE_CURVE('',#6255,#6123,#3846,.T.);
#7862=EDGE_CURVE('',#6137,#6256,#3847,.T.);
#7863=EDGE_CURVE('',#6256,#6257,#3848,.T.);
#7864=EDGE_CURVE('',#6257,#6142,#3849,.T.);
#7865=EDGE_CURVE('',#6258,#6259,#3850,.T.);
#7866=EDGE_CURVE('',#6259,#6257,#1243,.T.);
#7867=EDGE_CURVE('',#6256,#6258,#1244,.T.);
#7868=EDGE_CURVE('',#6153,#6259,#3851,.T.);
#7869=EDGE_CURVE('',#6258,#6148,#3852,.T.);
#7870=EDGE_CURVE('',#6107,#6260,#3853,.T.);
#7871=EDGE_CURVE('',#6260,#6261,#3854,.T.);
#7872=EDGE_CURVE('',#6261,#6248,#3855,.T.);
#7873=EDGE_CURVE('',#6262,#6263,#3856,.T.);
#7874=EDGE_CURVE('',#6263,#6261,#1245,.T.);
#7875=EDGE_CURVE('',#6260,#6262,#1246,.T.);
#7876=EDGE_CURVE('',#6255,#6263,#3857,.T.);
#7877=EDGE_CURVE('',#6262,#6124,#3858,.T.);
#7878=EDGE_CURVE('',#6159,#6264,#3859,.T.);
#7879=EDGE_CURVE('',#6264,#6265,#3860,.T.);
#7880=EDGE_CURVE('',#6265,#6152,#3861,.T.);
#7881=EDGE_CURVE('',#6203,#6266,#3862,.T.);
#7882=EDGE_CURVE('',#6266,#6265,#1247,.T.);
#7883=EDGE_CURVE('',#6264,#6203,#1248,.T.);
#7884=EDGE_CURVE('',#6192,#6266,#3863,.T.);
#7885=EDGE_CURVE('',#6178,#6267,#3864,.T.);
#7886=EDGE_CURVE('',#6267,#6246,#3865,.T.);
#7887=EDGE_CURVE('',#6268,#6269,#3866,.T.);
#7888=EDGE_CURVE('',#6269,#6267,#1249,.T.);
#7889=EDGE_CURVE('',#6178,#6268,#1250,.T.);
#7890=EDGE_CURVE('',#6249,#6269,#3867,.T.);
#7891=EDGE_CURVE('',#6268,#6116,#3868,.T.);
#7892=EDGE_CURVE('',#6270,#6205,#3869,.T.);
#7893=EDGE_CURVE('',#6247,#6270,#1251,.T.);
#7894=EDGE_CURVE('',#6271,#6204,#3870,.T.);
#7895=EDGE_CURVE('',#6270,#6271,#3871,.T.);
#7896=EDGE_CURVE('',#6271,#6191,#1252,.T.);
#7897=EDGE_CURVE('',#6272,#6264,#3872,.T.);
#7898=EDGE_CURVE('',#6200,#6272,#1253,.T.);
#7899=EDGE_CURVE('',#6272,#6158,#3873,.T.);
#7900=EDGE_CURVE('',#6273,#6258,#3874,.T.);
#7901=EDGE_CURVE('',#6149,#6273,#3875,.T.);
#7902=EDGE_CURVE('',#6274,#6256,#3876,.T.);
#7903=EDGE_CURVE('',#6273,#6274,#1254,.T.);
#7904=EDGE_CURVE('',#6274,#6136,#3877,.T.);
#7905=EDGE_CURVE('',#6138,#6275,#1255,.T.);
#7906=EDGE_CURVE('',#6275,#6228,#3878,.T.);
#7907=EDGE_CURVE('',#6275,#6276,#3879,.T.);
#7908=EDGE_CURVE('',#6276,#6226,#3880,.T.);
#7909=EDGE_CURVE('',#6276,#6126,#1256,.T.);
#7910=EDGE_CURVE('',#6273,#6234,#3881,.T.);
#7911=EDGE_CURVE('',#6274,#6232,#3882,.T.);
#7912=EDGE_CURVE('',#6130,#6110,#1257,.T.);
#7913=EDGE_CURVE('',#6272,#6238,#3883,.T.);
#7914=EDGE_CURVE('',#6118,#6177,#1258,.T.);
#7915=EDGE_CURVE('',#6276,#6253,#3884,.T.);
#7916=EDGE_CURVE('',#6251,#6275,#3885,.T.);
#7917=EDGE_CURVE('',#6118,#6268,#3886,.T.);
#7918=EDGE_CURVE('',#6130,#6262,#3887,.T.);
#7919=EDGE_CURVE('',#6110,#6260,#3888,.T.);
#10019=ORIENTED_EDGE('',*,*,#7625,.T.);
#10020=ORIENTED_EDGE('',*,*,#7626,.T.);
#10021=ORIENTED_EDGE('',*,*,#7627,.T.);
#10022=ORIENTED_EDGE('',*,*,#7628,.T.);
#10023=ORIENTED_EDGE('',*,*,#7629,.T.);
#10024=ORIENTED_EDGE('',*,*,#7630,.T.);
#10025=ORIENTED_EDGE('',*,*,#7628,.F.);
#10026=ORIENTED_EDGE('',*,*,#7631,.F.);
#10027=ORIENTED_EDGE('',*,*,#7632,.F.);
#10028=ORIENTED_EDGE('',*,*,#7633,.F.);
#10029=ORIENTED_EDGE('',*,*,#7634,.T.);
#10030=ORIENTED_EDGE('',*,*,#7627,.F.);
#10031=ORIENTED_EDGE('',*,*,#7635,.T.);
#10032=ORIENTED_EDGE('',*,*,#7636,.F.);
#10033=ORIENTED_EDGE('',*,*,#7637,.F.);
#10034=ORIENTED_EDGE('',*,*,#7638,.F.);
#10035=ORIENTED_EDGE('',*,*,#7631,.T.);
#10036=ORIENTED_EDGE('',*,*,#7626,.F.);
#10037=ORIENTED_EDGE('',*,*,#7639,.F.);
#10038=ORIENTED_EDGE('',*,*,#7640,.F.);
#10039=ORIENTED_EDGE('',*,*,#7635,.F.);
#10040=ORIENTED_EDGE('',*,*,#7636,.T.);
#10041=ORIENTED_EDGE('',*,*,#7640,.T.);
#10042=ORIENTED_EDGE('',*,*,#7641,.T.);
#10043=ORIENTED_EDGE('',*,*,#7642,.T.);
#10044=ORIENTED_EDGE('',*,*,#7643,.T.);
#10045=ORIENTED_EDGE('',*,*,#7644,.T.);
#10046=ORIENTED_EDGE('',*,*,#7644,.F.);
#10047=ORIENTED_EDGE('',*,*,#7645,.T.);
#10048=ORIENTED_EDGE('',*,*,#7646,.T.);
#10049=ORIENTED_EDGE('',*,*,#7647,.F.);
#10050=ORIENTED_EDGE('',*,*,#7637,.T.);
#10051=ORIENTED_EDGE('',*,*,#7648,.T.);
#10052=ORIENTED_EDGE('',*,*,#7649,.T.);
#10053=ORIENTED_EDGE('',*,*,#7650,.T.);
#10054=ORIENTED_EDGE('',*,*,#7651,.T.);
#10055=ORIENTED_EDGE('',*,*,#7652,.T.);
#10056=ORIENTED_EDGE('',*,*,#7653,.T.);
#10057=ORIENTED_EDGE('',*,*,#7649,.F.);
#10058=ORIENTED_EDGE('',*,*,#7654,.F.);
#10059=ORIENTED_EDGE('',*,*,#7655,.F.);
#10060=ORIENTED_EDGE('',*,*,#7656,.F.);
#10061=ORIENTED_EDGE('',*,*,#7648,.F.);
#10062=ORIENTED_EDGE('',*,*,#7657,.F.);
#10063=ORIENTED_EDGE('',*,*,#7658,.F.);
#10064=ORIENTED_EDGE('',*,*,#7659,.F.);
#10065=ORIENTED_EDGE('',*,*,#7654,.T.);
#10066=ORIENTED_EDGE('',*,*,#7653,.F.);
#10067=ORIENTED_EDGE('',*,*,#7660,.T.);
#10068=ORIENTED_EDGE('',*,*,#7661,.T.);
#10069=ORIENTED_EDGE('',*,*,#7662,.F.);
#10070=ORIENTED_EDGE('',*,*,#7657,.T.);
#10071=ORIENTED_EDGE('',*,*,#7663,.T.);
#10072=ORIENTED_EDGE('',*,*,#7664,.T.);
#10073=ORIENTED_EDGE('',*,*,#7665,.T.);
#10074=ORIENTED_EDGE('',*,*,#7666,.T.);
#10075=ORIENTED_EDGE('',*,*,#7667,.T.);
#10076=ORIENTED_EDGE('',*,*,#7668,.T.);
#10077=ORIENTED_EDGE('',*,*,#7665,.F.);
#10078=ORIENTED_EDGE('',*,*,#7669,.T.);
#10079=ORIENTED_EDGE('',*,*,#7670,.T.);
#10080=ORIENTED_EDGE('',*,*,#7671,.F.);
#10081=ORIENTED_EDGE('',*,*,#7672,.T.);
#10082=ORIENTED_EDGE('',*,*,#7664,.F.);
#10083=ORIENTED_EDGE('',*,*,#7673,.F.);
#10084=ORIENTED_EDGE('',*,*,#7674,.F.);
#10085=ORIENTED_EDGE('',*,*,#7669,.F.);
#10086=ORIENTED_EDGE('',*,*,#7663,.F.);
#10087=ORIENTED_EDGE('',*,*,#7675,.T.);
#10088=ORIENTED_EDGE('',*,*,#7676,.T.);
#10089=ORIENTED_EDGE('',*,*,#7677,.T.);
#10090=ORIENTED_EDGE('',*,*,#7673,.T.);
#10091=ORIENTED_EDGE('',*,*,#7678,.T.);
#10092=ORIENTED_EDGE('',*,*,#7679,.T.);
#10093=ORIENTED_EDGE('',*,*,#7680,.T.);
#10094=ORIENTED_EDGE('',*,*,#7681,.T.);
#10095=ORIENTED_EDGE('',*,*,#7682,.T.);
#10096=ORIENTED_EDGE('',*,*,#7683,.T.);
#10097=ORIENTED_EDGE('',*,*,#7680,.F.);
#10098=ORIENTED_EDGE('',*,*,#7684,.T.);
#10099=ORIENTED_EDGE('',*,*,#7685,.F.);
#10100=ORIENTED_EDGE('',*,*,#7686,.T.);
#10101=ORIENTED_EDGE('',*,*,#7687,.T.);
#10102=ORIENTED_EDGE('',*,*,#7688,.T.);
#10103=ORIENTED_EDGE('',*,*,#7679,.F.);
#10104=ORIENTED_EDGE('',*,*,#7689,.F.);
#10105=ORIENTED_EDGE('',*,*,#7690,.F.);
#10106=ORIENTED_EDGE('',*,*,#7684,.F.);
#10107=ORIENTED_EDGE('',*,*,#7678,.F.);
#10108=ORIENTED_EDGE('',*,*,#7691,.F.);
#10109=ORIENTED_EDGE('',*,*,#7692,.F.);
#10110=ORIENTED_EDGE('',*,*,#7693,.T.);
#10111=ORIENTED_EDGE('',*,*,#7694,.F.);
#10112=ORIENTED_EDGE('',*,*,#7689,.T.);
#10113=ORIENTED_EDGE('',*,*,#7685,.T.);
#10114=ORIENTED_EDGE('',*,*,#7690,.T.);
#10115=ORIENTED_EDGE('',*,*,#7694,.T.);
#10116=ORIENTED_EDGE('',*,*,#7695,.T.);
#10117=ORIENTED_EDGE('',*,*,#7696,.T.);
#10118=ORIENTED_EDGE('',*,*,#7697,.T.);
#10119=ORIENTED_EDGE('',*,*,#7698,.T.);
#10120=ORIENTED_EDGE('',*,*,#7699,.T.);
#10121=ORIENTED_EDGE('',*,*,#7700,.T.);
#10122=ORIENTED_EDGE('',*,*,#7699,.F.);
#10123=ORIENTED_EDGE('',*,*,#7698,.F.);
#10124=ORIENTED_EDGE('',*,*,#7701,.T.);
#10125=ORIENTED_EDGE('',*,*,#7702,.F.);
#10126=ORIENTED_EDGE('',*,*,#7701,.F.);
#10127=ORIENTED_EDGE('',*,*,#7703,.F.);
#10128=ORIENTED_EDGE('',*,*,#7700,.F.);
#10129=ORIENTED_EDGE('',*,*,#7702,.T.);
#10130=ORIENTED_EDGE('',*,*,#7704,.T.);
#10131=ORIENTED_EDGE('',*,*,#7705,.T.);
#10132=ORIENTED_EDGE('',*,*,#7704,.F.);
#10133=ORIENTED_EDGE('',*,*,#7705,.F.);
#10134=ORIENTED_EDGE('',*,*,#7706,.T.);
#10135=ORIENTED_EDGE('',*,*,#7707,.T.);
#10136=ORIENTED_EDGE('',*,*,#7706,.F.);
#10137=ORIENTED_EDGE('',*,*,#7708,.F.);
#10138=ORIENTED_EDGE('',*,*,#7709,.T.);
#10139=ORIENTED_EDGE('',*,*,#7710,.T.);
#10140=ORIENTED_EDGE('',*,*,#7711,.T.);
#10141=ORIENTED_EDGE('',*,*,#7709,.F.);
#10142=ORIENTED_EDGE('',*,*,#7708,.T.);
#10143=ORIENTED_EDGE('',*,*,#7710,.F.);
#10144=ORIENTED_EDGE('',*,*,#7711,.F.);
#10145=ORIENTED_EDGE('',*,*,#7712,.T.);
#10146=ORIENTED_EDGE('',*,*,#7713,.F.);
#10147=ORIENTED_EDGE('',*,*,#7714,.F.);
#10148=ORIENTED_EDGE('',*,*,#7712,.F.);
#10149=ORIENTED_EDGE('',*,*,#7715,.T.);
#10150=ORIENTED_EDGE('',*,*,#7716,.T.);
#10151=ORIENTED_EDGE('',*,*,#7717,.T.);
#10152=ORIENTED_EDGE('',*,*,#7718,.T.);
#10153=ORIENTED_EDGE('',*,*,#7719,.T.);
#10154=ORIENTED_EDGE('',*,*,#7720,.T.);
#10155=ORIENTED_EDGE('',*,*,#7719,.F.);
#10156=ORIENTED_EDGE('',*,*,#7721,.F.);
#10157=ORIENTED_EDGE('',*,*,#7722,.T.);
#10158=ORIENTED_EDGE('',*,*,#7723,.F.);
#10159=ORIENTED_EDGE('',*,*,#7718,.F.);
#10160=ORIENTED_EDGE('',*,*,#7724,.F.);
#10161=ORIENTED_EDGE('',*,*,#7725,.F.);
#10162=ORIENTED_EDGE('',*,*,#7726,.F.);
#10163=ORIENTED_EDGE('',*,*,#7727,.F.);
#10164=ORIENTED_EDGE('',*,*,#7721,.T.);
#10165=ORIENTED_EDGE('',*,*,#7717,.F.);
#10166=ORIENTED_EDGE('',*,*,#7728,.T.);
#10167=ORIENTED_EDGE('',*,*,#7729,.T.);
#10168=ORIENTED_EDGE('',*,*,#7730,.T.);
#10169=ORIENTED_EDGE('',*,*,#7724,.T.);
#10170=ORIENTED_EDGE('',*,*,#7731,.T.);
#10171=ORIENTED_EDGE('',*,*,#7732,.T.);
#10172=ORIENTED_EDGE('',*,*,#7733,.T.);
#10173=ORIENTED_EDGE('',*,*,#7734,.T.);
#10174=ORIENTED_EDGE('',*,*,#7735,.T.);
#10175=ORIENTED_EDGE('',*,*,#7736,.T.);
#10176=ORIENTED_EDGE('',*,*,#7733,.F.);
#10177=ORIENTED_EDGE('',*,*,#7737,.T.);
#10178=ORIENTED_EDGE('',*,*,#7738,.F.);
#10179=ORIENTED_EDGE('',*,*,#7739,.T.);
#10180=ORIENTED_EDGE('',*,*,#7740,.T.);
#10181=ORIENTED_EDGE('',*,*,#7732,.F.);
#10182=ORIENTED_EDGE('',*,*,#7741,.F.);
#10183=ORIENTED_EDGE('',*,*,#7742,.F.);
#10184=ORIENTED_EDGE('',*,*,#7737,.F.);
#10185=ORIENTED_EDGE('',*,*,#7731,.F.);
#10186=ORIENTED_EDGE('',*,*,#7743,.T.);
#10187=ORIENTED_EDGE('',*,*,#7744,.T.);
#10188=ORIENTED_EDGE('',*,*,#7745,.F.);
#10189=ORIENTED_EDGE('',*,*,#7741,.T.);
#10190=ORIENTED_EDGE('',*,*,#7746,.T.);
#10191=ORIENTED_EDGE('',*,*,#7747,.T.);
#10192=ORIENTED_EDGE('',*,*,#7729,.F.);
#10193=ORIENTED_EDGE('',*,*,#7748,.T.);
#10194=ORIENTED_EDGE('',*,*,#7749,.T.);
#10195=ORIENTED_EDGE('',*,*,#7750,.T.);
#10196=ORIENTED_EDGE('',*,*,#7746,.F.);
#10197=ORIENTED_EDGE('',*,*,#7751,.T.);
#10198=ORIENTED_EDGE('',*,*,#7745,.T.);
#10199=ORIENTED_EDGE('',*,*,#7752,.T.);
#10200=ORIENTED_EDGE('',*,*,#7749,.F.);
#10201=ORIENTED_EDGE('',*,*,#7753,.T.);
#10202=ORIENTED_EDGE('',*,*,#7736,.F.);
#10203=ORIENTED_EDGE('',*,*,#7754,.T.);
#10204=ORIENTED_EDGE('',*,*,#7755,.T.);
#10205=ORIENTED_EDGE('',*,*,#7756,.F.);
#10206=ORIENTED_EDGE('',*,*,#7757,.T.);
#10207=ORIENTED_EDGE('',*,*,#7743,.F.);
#10208=ORIENTED_EDGE('',*,*,#7735,.F.);
#10209=ORIENTED_EDGE('',*,*,#7758,.F.);
#10210=ORIENTED_EDGE('',*,*,#7759,.F.);
#10211=ORIENTED_EDGE('',*,*,#7754,.F.);
#10212=ORIENTED_EDGE('',*,*,#7753,.F.);
#10213=ORIENTED_EDGE('',*,*,#7760,.T.);
#10214=ORIENTED_EDGE('',*,*,#7761,.F.);
#10215=ORIENTED_EDGE('',*,*,#7742,.T.);
#10216=ORIENTED_EDGE('',*,*,#7751,.F.);
#10217=ORIENTED_EDGE('',*,*,#7762,.F.);
#10218=ORIENTED_EDGE('',*,*,#7763,.F.);
#10219=ORIENTED_EDGE('',*,*,#7760,.F.);
#10220=ORIENTED_EDGE('',*,*,#7748,.F.);
#10221=ORIENTED_EDGE('',*,*,#7764,.T.);
#10222=ORIENTED_EDGE('',*,*,#7765,.F.);
#10223=ORIENTED_EDGE('',*,*,#7762,.T.);
#10224=ORIENTED_EDGE('',*,*,#7716,.F.);
#10225=ORIENTED_EDGE('',*,*,#7766,.F.);
#10226=ORIENTED_EDGE('',*,*,#7764,.F.);
#10227=ORIENTED_EDGE('',*,*,#7728,.F.);
#10228=ORIENTED_EDGE('',*,*,#7767,.T.);
#10229=ORIENTED_EDGE('',*,*,#7768,.T.);
#10230=ORIENTED_EDGE('',*,*,#7769,.T.);
#10231=ORIENTED_EDGE('',*,*,#7770,.T.);
#10232=ORIENTED_EDGE('',*,*,#7771,.T.);
#10233=ORIENTED_EDGE('',*,*,#7772,.T.);
#10234=ORIENTED_EDGE('',*,*,#7769,.F.);
#10235=ORIENTED_EDGE('',*,*,#7773,.T.);
#10236=ORIENTED_EDGE('',*,*,#7774,.T.);
#10237=ORIENTED_EDGE('',*,*,#7775,.T.);
#10238=ORIENTED_EDGE('',*,*,#7771,.F.);
#10239=ORIENTED_EDGE('',*,*,#7776,.T.);
#10240=ORIENTED_EDGE('',*,*,#7777,.T.);
#10241=ORIENTED_EDGE('',*,*,#7778,.T.);
#10242=ORIENTED_EDGE('',*,*,#7774,.F.);
#10243=ORIENTED_EDGE('',*,*,#7779,.T.);
#10244=ORIENTED_EDGE('',*,*,#7780,.T.);
#10245=ORIENTED_EDGE('',*,*,#7781,.T.);
#10246=ORIENTED_EDGE('',*,*,#7777,.F.);
#10247=ORIENTED_EDGE('',*,*,#7782,.T.);
#10248=ORIENTED_EDGE('',*,*,#7744,.F.);
#10249=ORIENTED_EDGE('',*,*,#7757,.F.);
#10250=ORIENTED_EDGE('',*,*,#7770,.F.);
#10251=ORIENTED_EDGE('',*,*,#7783,.F.);
#10252=ORIENTED_EDGE('',*,*,#7752,.F.);
#10253=ORIENTED_EDGE('',*,*,#7783,.T.);
#10254=ORIENTED_EDGE('',*,*,#7772,.F.);
#10255=ORIENTED_EDGE('',*,*,#7784,.F.);
#10256=ORIENTED_EDGE('',*,*,#7750,.F.);
#10257=ORIENTED_EDGE('',*,*,#7784,.T.);
#10258=ORIENTED_EDGE('',*,*,#7775,.F.);
#10259=ORIENTED_EDGE('',*,*,#7785,.F.);
#10260=ORIENTED_EDGE('',*,*,#7747,.F.);
#10261=ORIENTED_EDGE('',*,*,#7785,.T.);
#10262=ORIENTED_EDGE('',*,*,#7778,.F.);
#10263=ORIENTED_EDGE('',*,*,#7786,.F.);
#10264=ORIENTED_EDGE('',*,*,#7730,.F.);
#10265=ORIENTED_EDGE('',*,*,#7786,.T.);
#10266=ORIENTED_EDGE('',*,*,#7781,.F.);
#10267=ORIENTED_EDGE('',*,*,#7725,.T.);
#10268=ORIENTED_EDGE('',*,*,#7780,.F.);
#10269=ORIENTED_EDGE('',*,*,#7787,.T.);
#10270=ORIENTED_EDGE('',*,*,#7788,.T.);
#10271=ORIENTED_EDGE('',*,*,#7726,.T.);
#10272=ORIENTED_EDGE('',*,*,#7789,.T.);
#10273=ORIENTED_EDGE('',*,*,#7790,.T.);
#10274=ORIENTED_EDGE('',*,*,#7788,.F.);
#10275=ORIENTED_EDGE('',*,*,#7791,.T.);
#10276=ORIENTED_EDGE('',*,*,#7647,.T.);
#10277=ORIENTED_EDGE('',*,*,#7789,.F.);
#10278=ORIENTED_EDGE('',*,*,#7792,.T.);
#10279=ORIENTED_EDGE('',*,*,#7793,.T.);
#10280=ORIENTED_EDGE('',*,*,#7794,.T.);
#10281=ORIENTED_EDGE('',*,*,#7795,.T.);
#10282=ORIENTED_EDGE('',*,*,#7638,.T.);
#10283=ORIENTED_EDGE('',*,*,#7793,.F.);
#10284=ORIENTED_EDGE('',*,*,#7796,.T.);
#10285=ORIENTED_EDGE('',*,*,#7797,.T.);
#10286=ORIENTED_EDGE('',*,*,#7632,.T.);
#10287=ORIENTED_EDGE('',*,*,#7795,.F.);
#10288=ORIENTED_EDGE('',*,*,#7798,.T.);
#10289=ORIENTED_EDGE('',*,*,#7799,.T.);
#10290=ORIENTED_EDGE('',*,*,#7797,.F.);
#10291=ORIENTED_EDGE('',*,*,#7800,.T.);
#10292=ORIENTED_EDGE('',*,*,#7662,.T.);
#10293=ORIENTED_EDGE('',*,*,#7798,.F.);
#10294=ORIENTED_EDGE('',*,*,#7801,.T.);
#10295=ORIENTED_EDGE('',*,*,#7802,.T.);
#10296=ORIENTED_EDGE('',*,*,#7803,.T.);
#10297=ORIENTED_EDGE('',*,*,#7804,.T.);
#10298=ORIENTED_EDGE('',*,*,#7658,.T.);
#10299=ORIENTED_EDGE('',*,*,#7802,.F.);
#10300=ORIENTED_EDGE('',*,*,#7805,.T.);
#10301=ORIENTED_EDGE('',*,*,#7806,.T.);
#10302=ORIENTED_EDGE('',*,*,#7804,.F.);
#10303=ORIENTED_EDGE('',*,*,#7807,.T.);
#10304=ORIENTED_EDGE('',*,*,#7808,.T.);
#10305=ORIENTED_EDGE('',*,*,#7809,.T.);
#10306=ORIENTED_EDGE('',*,*,#7805,.F.);
#10307=ORIENTED_EDGE('',*,*,#7810,.T.);
#10308=ORIENTED_EDGE('',*,*,#7811,.T.);
#10309=ORIENTED_EDGE('',*,*,#7812,.T.);
#10310=ORIENTED_EDGE('',*,*,#7808,.F.);
#10311=ORIENTED_EDGE('',*,*,#7813,.T.);
#10312=ORIENTED_EDGE('',*,*,#7671,.T.);
#10313=ORIENTED_EDGE('',*,*,#7811,.F.);
#10314=ORIENTED_EDGE('',*,*,#7814,.T.);
#10315=ORIENTED_EDGE('',*,*,#7815,.T.);
#10316=ORIENTED_EDGE('',*,*,#7816,.T.);
#10317=ORIENTED_EDGE('',*,*,#7817,.T.);
#10318=ORIENTED_EDGE('',*,*,#7818,.T.);
#10319=ORIENTED_EDGE('',*,*,#7815,.F.);
#10320=ORIENTED_EDGE('',*,*,#7819,.T.);
#10321=ORIENTED_EDGE('',*,*,#7820,.T.);
#10322=ORIENTED_EDGE('',*,*,#7817,.F.);
#10323=ORIENTED_EDGE('',*,*,#7821,.T.);
#10324=ORIENTED_EDGE('',*,*,#7822,.T.);
#10325=ORIENTED_EDGE('',*,*,#7819,.F.);
#10326=ORIENTED_EDGE('',*,*,#7823,.T.);
#10327=ORIENTED_EDGE('',*,*,#7824,.T.);
#10328=ORIENTED_EDGE('',*,*,#7825,.T.);
#10329=ORIENTED_EDGE('',*,*,#7826,.T.);
#10330=ORIENTED_EDGE('',*,*,#7692,.T.);
#10331=ORIENTED_EDGE('',*,*,#7824,.F.);
#10332=ORIENTED_EDGE('',*,*,#7827,.T.);
#10333=ORIENTED_EDGE('',*,*,#7828,.T.);
#10334=ORIENTED_EDGE('',*,*,#7829,.T.);
#10335=ORIENTED_EDGE('',*,*,#7826,.F.);
#10336=ORIENTED_EDGE('',*,*,#7830,.T.);
#10337=ORIENTED_EDGE('',*,*,#7831,.T.);
#10338=ORIENTED_EDGE('',*,*,#7828,.F.);
#10339=ORIENTED_EDGE('',*,*,#7832,.T.);
#10340=ORIENTED_EDGE('',*,*,#7767,.F.);
#10341=ORIENTED_EDGE('',*,*,#7756,.T.);
#10342=ORIENTED_EDGE('',*,*,#7830,.F.);
#10343=ORIENTED_EDGE('',*,*,#7833,.T.);
#10344=ORIENTED_EDGE('',*,*,#7768,.F.);
#10345=ORIENTED_EDGE('',*,*,#7833,.F.);
#10346=ORIENTED_EDGE('',*,*,#7832,.F.);
#10347=ORIENTED_EDGE('',*,*,#7827,.F.);
#10348=ORIENTED_EDGE('',*,*,#7825,.F.);
#10349=ORIENTED_EDGE('',*,*,#7823,.F.);
#10350=ORIENTED_EDGE('',*,*,#7821,.F.);
#10351=ORIENTED_EDGE('',*,*,#7816,.F.);
#10352=ORIENTED_EDGE('',*,*,#7814,.F.);
#10353=ORIENTED_EDGE('',*,*,#7813,.F.);
#10354=ORIENTED_EDGE('',*,*,#7810,.F.);
#10355=ORIENTED_EDGE('',*,*,#7807,.F.);
#10356=ORIENTED_EDGE('',*,*,#7803,.F.);
#10357=ORIENTED_EDGE('',*,*,#7801,.F.);
#10358=ORIENTED_EDGE('',*,*,#7800,.F.);
#10359=ORIENTED_EDGE('',*,*,#7796,.F.);
#10360=ORIENTED_EDGE('',*,*,#7794,.F.);
#10361=ORIENTED_EDGE('',*,*,#7792,.F.);
#10362=ORIENTED_EDGE('',*,*,#7791,.F.);
#10363=ORIENTED_EDGE('',*,*,#7787,.F.);
#10364=ORIENTED_EDGE('',*,*,#7782,.F.);
#10365=ORIENTED_EDGE('',*,*,#7779,.F.);
#10366=ORIENTED_EDGE('',*,*,#7776,.F.);
#10367=ORIENTED_EDGE('',*,*,#7773,.F.);
#10368=ORIENTED_EDGE('',*,*,#7834,.F.);
#10369=ORIENTED_EDGE('',*,*,#7835,.T.);
#10370=ORIENTED_EDGE('',*,*,#7713,.T.);
#10371=ORIENTED_EDGE('',*,*,#7714,.T.);
#10372=ORIENTED_EDGE('',*,*,#7835,.F.);
#10373=ORIENTED_EDGE('',*,*,#7836,.T.);
#10374=ORIENTED_EDGE('',*,*,#7837,.F.);
#10375=ORIENTED_EDGE('',*,*,#7838,.T.);
#10376=ORIENTED_EDGE('',*,*,#7839,.F.);
#10377=ORIENTED_EDGE('',*,*,#7840,.F.);
#10378=ORIENTED_EDGE('',*,*,#7838,.F.);
#10379=ORIENTED_EDGE('',*,*,#7836,.F.);
#10380=ORIENTED_EDGE('',*,*,#7841,.T.);
#10381=ORIENTED_EDGE('',*,*,#7842,.T.);
#10382=ORIENTED_EDGE('',*,*,#7837,.T.);
#10383=ORIENTED_EDGE('',*,*,#7842,.F.);
#10384=ORIENTED_EDGE('',*,*,#7703,.T.);
#10385=ORIENTED_EDGE('',*,*,#7843,.T.);
#10386=ORIENTED_EDGE('',*,*,#7841,.F.);
#10387=ORIENTED_EDGE('',*,*,#7843,.F.);
#10388=ORIENTED_EDGE('',*,*,#7840,.T.);
#10389=ORIENTED_EDGE('',*,*,#7844,.T.);
#10390=ORIENTED_EDGE('',*,*,#7834,.T.);
#10391=ORIENTED_EDGE('',*,*,#7844,.F.);
#10392=ORIENTED_EDGE('',*,*,#7839,.T.);
#10393=ORIENTED_EDGE('',*,*,#7707,.F.);
#10394=ORIENTED_EDGE('',*,*,#7715,.F.);
#10395=ORIENTED_EDGE('',*,*,#7845,.T.);
#10396=ORIENTED_EDGE('',*,*,#7846,.T.);
#10397=ORIENTED_EDGE('',*,*,#7847,.T.);
#10398=ORIENTED_EDGE('',*,*,#7766,.T.);
#10399=ORIENTED_EDGE('',*,*,#7625,.F.);
#10400=ORIENTED_EDGE('',*,*,#7848,.T.);
#10401=ORIENTED_EDGE('',*,*,#7849,.T.);
#10402=ORIENTED_EDGE('',*,*,#7850,.T.);
#10403=ORIENTED_EDGE('',*,*,#7641,.F.);
#10404=ORIENTED_EDGE('',*,*,#7639,.T.);
#10405=ORIENTED_EDGE('',*,*,#7851,.T.);
#10406=ORIENTED_EDGE('',*,*,#7852,.T.);
#10407=ORIENTED_EDGE('',*,*,#7677,.F.);
#10408=ORIENTED_EDGE('',*,*,#7853,.T.);
#10409=ORIENTED_EDGE('',*,*,#7854,.T.);
#10410=ORIENTED_EDGE('',*,*,#7855,.T.);
#10411=ORIENTED_EDGE('',*,*,#7851,.F.);
#10412=ORIENTED_EDGE('',*,*,#7856,.T.);
#10413=ORIENTED_EDGE('',*,*,#7857,.T.);
#10414=ORIENTED_EDGE('',*,*,#7858,.T.);
#10415=ORIENTED_EDGE('',*,*,#7854,.F.);
#10416=ORIENTED_EDGE('',*,*,#7859,.T.);
#10417=ORIENTED_EDGE('',*,*,#7650,.F.);
#10418=ORIENTED_EDGE('',*,*,#7656,.T.);
#10419=ORIENTED_EDGE('',*,*,#7857,.F.);
#10420=ORIENTED_EDGE('',*,*,#7860,.T.);
#10421=ORIENTED_EDGE('',*,*,#7861,.T.);
#10422=ORIENTED_EDGE('',*,*,#7668,.F.);
#10423=ORIENTED_EDGE('',*,*,#7862,.T.);
#10424=ORIENTED_EDGE('',*,*,#7863,.T.);
#10425=ORIENTED_EDGE('',*,*,#7864,.T.);
#10426=ORIENTED_EDGE('',*,*,#7675,.F.);
#10427=ORIENTED_EDGE('',*,*,#7865,.T.);
#10428=ORIENTED_EDGE('',*,*,#7866,.T.);
#10429=ORIENTED_EDGE('',*,*,#7863,.F.);
#10430=ORIENTED_EDGE('',*,*,#7867,.T.);
#10431=ORIENTED_EDGE('',*,*,#7681,.F.);
#10432=ORIENTED_EDGE('',*,*,#7688,.F.);
#10433=ORIENTED_EDGE('',*,*,#7868,.T.);
#10434=ORIENTED_EDGE('',*,*,#7865,.F.);
#10435=ORIENTED_EDGE('',*,*,#7869,.T.);
#10436=ORIENTED_EDGE('',*,*,#7630,.F.);
#10437=ORIENTED_EDGE('',*,*,#7870,.T.);
#10438=ORIENTED_EDGE('',*,*,#7871,.T.);
#10439=ORIENTED_EDGE('',*,*,#7872,.T.);
#10440=ORIENTED_EDGE('',*,*,#7848,.F.);
#10441=ORIENTED_EDGE('',*,*,#7873,.T.);
#10442=ORIENTED_EDGE('',*,*,#7874,.T.);
#10443=ORIENTED_EDGE('',*,*,#7871,.F.);
#10444=ORIENTED_EDGE('',*,*,#7875,.T.);
#10445=ORIENTED_EDGE('',*,*,#7651,.F.);
#10446=ORIENTED_EDGE('',*,*,#7861,.F.);
#10447=ORIENTED_EDGE('',*,*,#7876,.T.);
#10448=ORIENTED_EDGE('',*,*,#7873,.F.);
#10449=ORIENTED_EDGE('',*,*,#7877,.T.);
#10450=ORIENTED_EDGE('',*,*,#7697,.F.);
#10451=ORIENTED_EDGE('',*,*,#7878,.T.);
#10452=ORIENTED_EDGE('',*,*,#7879,.T.);
#10453=ORIENTED_EDGE('',*,*,#7880,.T.);
#10454=ORIENTED_EDGE('',*,*,#7686,.F.);
#10455=ORIENTED_EDGE('',*,*,#7881,.T.);
#10456=ORIENTED_EDGE('',*,*,#7882,.T.);
#10457=ORIENTED_EDGE('',*,*,#7879,.F.);
#10458=ORIENTED_EDGE('',*,*,#7883,.T.);
#10459=ORIENTED_EDGE('',*,*,#7734,.F.);
#10460=ORIENTED_EDGE('',*,*,#7740,.F.);
#10461=ORIENTED_EDGE('',*,*,#7884,.T.);
#10462=ORIENTED_EDGE('',*,*,#7881,.F.);
#10463=ORIENTED_EDGE('',*,*,#7758,.T.);
#10464=ORIENTED_EDGE('',*,*,#7720,.F.);
#10465=ORIENTED_EDGE('',*,*,#7723,.T.);
#10466=ORIENTED_EDGE('',*,*,#7885,.T.);
#10467=ORIENTED_EDGE('',*,*,#7886,.T.);
#10468=ORIENTED_EDGE('',*,*,#7845,.F.);
#10469=ORIENTED_EDGE('',*,*,#7887,.T.);
#10470=ORIENTED_EDGE('',*,*,#7888,.T.);
#10471=ORIENTED_EDGE('',*,*,#7885,.F.);
#10472=ORIENTED_EDGE('',*,*,#7889,.T.);
#10473=ORIENTED_EDGE('',*,*,#7642,.F.);
#10474=ORIENTED_EDGE('',*,*,#7850,.F.);
#10475=ORIENTED_EDGE('',*,*,#7890,.T.);
#10476=ORIENTED_EDGE('',*,*,#7887,.F.);
#10477=ORIENTED_EDGE('',*,*,#7891,.T.);
#10478=ORIENTED_EDGE('',*,*,#7892,.T.);
#10479=ORIENTED_EDGE('',*,*,#7765,.T.);
#10480=ORIENTED_EDGE('',*,*,#7847,.F.);
#10481=ORIENTED_EDGE('',*,*,#7893,.T.);
#10482=ORIENTED_EDGE('',*,*,#7894,.T.);
#10483=ORIENTED_EDGE('',*,*,#7763,.T.);
#10484=ORIENTED_EDGE('',*,*,#7892,.F.);
#10485=ORIENTED_EDGE('',*,*,#7895,.T.);
#10486=ORIENTED_EDGE('',*,*,#7738,.T.);
#10487=ORIENTED_EDGE('',*,*,#7761,.T.);
#10488=ORIENTED_EDGE('',*,*,#7894,.F.);
#10489=ORIENTED_EDGE('',*,*,#7896,.T.);
#10490=ORIENTED_EDGE('',*,*,#7883,.F.);
#10491=ORIENTED_EDGE('',*,*,#7897,.F.);
#10492=ORIENTED_EDGE('',*,*,#7898,.F.);
#10493=ORIENTED_EDGE('',*,*,#7759,.T.);
#10494=ORIENTED_EDGE('',*,*,#7696,.F.);
#10495=ORIENTED_EDGE('',*,*,#7899,.F.);
#10496=ORIENTED_EDGE('',*,*,#7897,.T.);
#10497=ORIENTED_EDGE('',*,*,#7878,.F.);
#10498=ORIENTED_EDGE('',*,*,#7682,.F.);
#10499=ORIENTED_EDGE('',*,*,#7869,.F.);
#10500=ORIENTED_EDGE('',*,*,#7900,.F.);
#10501=ORIENTED_EDGE('',*,*,#7901,.F.);
#10502=ORIENTED_EDGE('',*,*,#7867,.F.);
#10503=ORIENTED_EDGE('',*,*,#7902,.F.);
#10504=ORIENTED_EDGE('',*,*,#7903,.F.);
#10505=ORIENTED_EDGE('',*,*,#7900,.T.);
#10506=ORIENTED_EDGE('',*,*,#7667,.F.);
#10507=ORIENTED_EDGE('',*,*,#7904,.F.);
#10508=ORIENTED_EDGE('',*,*,#7902,.T.);
#10509=ORIENTED_EDGE('',*,*,#7862,.F.);
#10510=ORIENTED_EDGE('',*,*,#7676,.F.);
#10511=ORIENTED_EDGE('',*,*,#7864,.F.);
#10512=ORIENTED_EDGE('',*,*,#7866,.F.);
#10513=ORIENTED_EDGE('',*,*,#7868,.F.);
#10514=ORIENTED_EDGE('',*,*,#7687,.F.);
#10515=ORIENTED_EDGE('',*,*,#7880,.F.);
#10516=ORIENTED_EDGE('',*,*,#7882,.F.);
#10517=ORIENTED_EDGE('',*,*,#7884,.F.);
#10518=ORIENTED_EDGE('',*,*,#7739,.F.);
#10519=ORIENTED_EDGE('',*,*,#7896,.F.);
#10520=ORIENTED_EDGE('',*,*,#7895,.F.);
#10521=ORIENTED_EDGE('',*,*,#7893,.F.);
#10522=ORIENTED_EDGE('',*,*,#7846,.F.);
#10523=ORIENTED_EDGE('',*,*,#7886,.F.);
#10524=ORIENTED_EDGE('',*,*,#7888,.F.);
#10525=ORIENTED_EDGE('',*,*,#7890,.F.);
#10526=ORIENTED_EDGE('',*,*,#7849,.F.);
#10527=ORIENTED_EDGE('',*,*,#7872,.F.);
#10528=ORIENTED_EDGE('',*,*,#7874,.F.);
#10529=ORIENTED_EDGE('',*,*,#7876,.F.);
#10530=ORIENTED_EDGE('',*,*,#7860,.F.);
#10531=ORIENTED_EDGE('',*,*,#7859,.F.);
#10532=ORIENTED_EDGE('',*,*,#7856,.F.);
#10533=ORIENTED_EDGE('',*,*,#7853,.F.);
#10534=ORIENTED_EDGE('',*,*,#7812,.F.);
#10535=ORIENTED_EDGE('',*,*,#7670,.F.);
#10536=ORIENTED_EDGE('',*,*,#7905,.T.);
#10537=ORIENTED_EDGE('',*,*,#7906,.T.);
#10538=ORIENTED_EDGE('',*,*,#7809,.F.);
#10539=ORIENTED_EDGE('',*,*,#7906,.F.);
#10540=ORIENTED_EDGE('',*,*,#7907,.T.);
#10541=ORIENTED_EDGE('',*,*,#7908,.T.);
#10542=ORIENTED_EDGE('',*,*,#7806,.F.);
#10543=ORIENTED_EDGE('',*,*,#7908,.F.);
#10544=ORIENTED_EDGE('',*,*,#7909,.T.);
#10545=ORIENTED_EDGE('',*,*,#7659,.T.);
#10546=ORIENTED_EDGE('',*,*,#7683,.F.);
#10547=ORIENTED_EDGE('',*,*,#7901,.T.);
#10548=ORIENTED_EDGE('',*,*,#7910,.T.);
#10549=ORIENTED_EDGE('',*,*,#7822,.F.);
#10550=ORIENTED_EDGE('',*,*,#7691,.T.);
#10551=ORIENTED_EDGE('',*,*,#7820,.F.);
#10552=ORIENTED_EDGE('',*,*,#7910,.F.);
#10553=ORIENTED_EDGE('',*,*,#7903,.T.);
#10554=ORIENTED_EDGE('',*,*,#7911,.T.);
#10555=ORIENTED_EDGE('',*,*,#7666,.F.);
#10556=ORIENTED_EDGE('',*,*,#7672,.F.);
#10557=ORIENTED_EDGE('',*,*,#7818,.F.);
#10558=ORIENTED_EDGE('',*,*,#7911,.F.);
#10559=ORIENTED_EDGE('',*,*,#7904,.T.);
#10560=ORIENTED_EDGE('',*,*,#7799,.F.);
#10561=ORIENTED_EDGE('',*,*,#7661,.F.);
#10562=ORIENTED_EDGE('',*,*,#7912,.T.);
#10563=ORIENTED_EDGE('',*,*,#7633,.T.);
#10564=ORIENTED_EDGE('',*,*,#7831,.F.);
#10565=ORIENTED_EDGE('',*,*,#7755,.F.);
#10566=ORIENTED_EDGE('',*,*,#7898,.T.);
#10567=ORIENTED_EDGE('',*,*,#7913,.T.);
#10568=ORIENTED_EDGE('',*,*,#7695,.F.);
#10569=ORIENTED_EDGE('',*,*,#7693,.F.);
#10570=ORIENTED_EDGE('',*,*,#7829,.F.);
#10571=ORIENTED_EDGE('',*,*,#7913,.F.);
#10572=ORIENTED_EDGE('',*,*,#7899,.T.);
#10573=ORIENTED_EDGE('',*,*,#7790,.F.);
#10574=ORIENTED_EDGE('',*,*,#7646,.F.);
#10575=ORIENTED_EDGE('',*,*,#7914,.T.);
#10576=ORIENTED_EDGE('',*,*,#7727,.T.);
#10577=ORIENTED_EDGE('',*,*,#7858,.F.);
#10578=ORIENTED_EDGE('',*,*,#7655,.T.);
#10579=ORIENTED_EDGE('',*,*,#7909,.F.);
#10580=ORIENTED_EDGE('',*,*,#7915,.T.);
#10581=ORIENTED_EDGE('',*,*,#7855,.F.);
#10582=ORIENTED_EDGE('',*,*,#7915,.F.);
#10583=ORIENTED_EDGE('',*,*,#7907,.F.);
#10584=ORIENTED_EDGE('',*,*,#7916,.F.);
#10585=ORIENTED_EDGE('',*,*,#7852,.F.);
#10586=ORIENTED_EDGE('',*,*,#7916,.T.);
#10587=ORIENTED_EDGE('',*,*,#7905,.F.);
#10588=ORIENTED_EDGE('',*,*,#7674,.T.);
#10589=ORIENTED_EDGE('',*,*,#7643,.F.);
#10590=ORIENTED_EDGE('',*,*,#7891,.F.);
#10591=ORIENTED_EDGE('',*,*,#7917,.F.);
#10592=ORIENTED_EDGE('',*,*,#7645,.F.);
#10593=ORIENTED_EDGE('',*,*,#7889,.F.);
#10594=ORIENTED_EDGE('',*,*,#7722,.F.);
#10595=ORIENTED_EDGE('',*,*,#7914,.F.);
#10596=ORIENTED_EDGE('',*,*,#7917,.T.);
#10597=ORIENTED_EDGE('',*,*,#7652,.F.);
#10598=ORIENTED_EDGE('',*,*,#7877,.F.);
#10599=ORIENTED_EDGE('',*,*,#7918,.F.);
#10600=ORIENTED_EDGE('',*,*,#7660,.F.);
#10601=ORIENTED_EDGE('',*,*,#7629,.F.);
#10602=ORIENTED_EDGE('',*,*,#7634,.F.);
#10603=ORIENTED_EDGE('',*,*,#7919,.T.);
#10604=ORIENTED_EDGE('',*,*,#7870,.F.);
#10605=ORIENTED_EDGE('',*,*,#7875,.F.);
#10606=ORIENTED_EDGE('',*,*,#7919,.F.);
#10607=ORIENTED_EDGE('',*,*,#7912,.F.);
#10608=ORIENTED_EDGE('',*,*,#7918,.T.);
#14807=PLANE('',#16405);
#14808=PLANE('',#16406);
#14809=PLANE('',#16407);
#14810=PLANE('',#16408);
#14811=PLANE('',#16409);
#14812=PLANE('',#16410);
#14813=PLANE('',#16411);
#14814=PLANE('',#16412);
#14815=PLANE('',#16413);
#14816=PLANE('',#16414);
#14817=PLANE('',#16415);
#14818=PLANE('',#16416);
#14819=PLANE('',#16417);
#14820=PLANE('',#16418);
#14821=PLANE('',#16419);
#14822=PLANE('',#16420);
#14823=PLANE('',#16421);
#14824=PLANE('',#16422);
#14825=PLANE('',#16423);
#14826=PLANE('',#16429);
#14827=PLANE('',#16436);
#14828=PLANE('',#16437);
#14829=PLANE('',#16438);
#14830=PLANE('',#16439);
#14831=PLANE('',#16440);
#14832=PLANE('',#16441);
#14833=PLANE('',#16442);
#14834=PLANE('',#16443);
#14835=PLANE('',#16447);
#14836=PLANE('',#16451);
#14837=PLANE('',#16452);
#14838=PLANE('',#16455);
#14839=PLANE('',#16458);
#14840=PLANE('',#16459);
#14841=PLANE('',#16463);
#14842=PLANE('',#16467);
#14843=PLANE('',#16468);
#14844=PLANE('',#16470);
#14845=PLANE('',#16472);
#14846=PLANE('',#16473);
#14847=PLANE('',#16477);
#14848=PLANE('',#16478);
#14849=PLANE('',#16479);
#14850=PLANE('',#16483);
#14851=PLANE('',#16484);
#14852=PLANE('',#16488);
#14853=PLANE('',#16492);
#14854=PLANE('',#16493);
#14855=PLANE('',#16497);
#14856=PLANE('',#16498);
#14857=PLANE('',#16499);
#14858=PLANE('',#16503);
#14859=PLANE('',#16504);
#14860=PLANE('',#16515);
#14861=PLANE('',#16516);
#14862=PLANE('',#16517);
#14863=PLANE('',#16521);
#14864=PLANE('',#16525);
#14865=PLANE('',#16526);
#14866=PLANE('',#16530);
#14867=PLANE('',#16531);
#14868=PLANE('',#16535);
#14869=PLANE('',#16536);
#14870=PLANE('',#16540);
#14871=PLANE('',#16541);
#14872=PLANE('',#16545);
#14873=PLANE('',#16548);
#14874=PLANE('',#16553);
#14875=PLANE('',#16554);
#14876=PLANE('',#16557);
#14877=PLANE('',#16558);
#14878=PLANE('',#16561);
#14879=PLANE('',#16564);
#14880=PLANE('',#16566);
#14881=PLANE('',#16570);
#14882=PLANE('',#16574);
#14883=PLANE('',#16576);
#14884=PLANE('',#16578);
#14885=PLANE('',#16579);
#15317=ADVANCED_FACE('',(#1774),#14807,.T.);
#15318=ADVANCED_FACE('',(#1775),#14808,.T.);
#15319=ADVANCED_FACE('',(#1776),#14809,.T.);
#15320=ADVANCED_FACE('',(#1777),#14810,.T.);
#15321=ADVANCED_FACE('',(#1778),#14811,.T.);
#15322=ADVANCED_FACE('',(#1779),#14812,.T.);
#15323=ADVANCED_FACE('',(#1780),#14813,.T.);
#15324=ADVANCED_FACE('',(#1781),#14814,.T.);
#15325=ADVANCED_FACE('',(#1782),#14815,.T.);
#15326=ADVANCED_FACE('',(#1783),#14816,.T.);
#15327=ADVANCED_FACE('',(#1784),#14817,.T.);
#15328=ADVANCED_FACE('',(#1785),#14818,.T.);
#15329=ADVANCED_FACE('',(#1786),#14819,.T.);
#15330=ADVANCED_FACE('',(#1787),#14820,.T.);
#15331=ADVANCED_FACE('',(#1788),#14821,.T.);
#15332=ADVANCED_FACE('',(#1789),#14822,.T.);
#15333=ADVANCED_FACE('',(#1790),#14823,.T.);
#15334=ADVANCED_FACE('',(#1791),#14824,.T.);
#15335=ADVANCED_FACE('',(#1792),#14825,.T.);
#15336=ADVANCED_FACE('',(#1793),#1672,.F.);
#15337=ADVANCED_FACE('',(#1794),#1673,.F.);
#15338=ADVANCED_FACE('',(#1795,#1159),#14826,.T.);
#15339=ADVANCED_FACE('',(#1796),#1674,.F.);
#15340=ADVANCED_FACE('',(#1797,#1160),#877,.F.);
#15341=ADVANCED_FACE('',(#1798),#490,.T.);
#15342=ADVANCED_FACE('',(#1799),#878,.F.);
#15343=ADVANCED_FACE('',(#1800),#14827,.T.);
#15344=ADVANCED_FACE('',(#1801),#14828,.F.);
#15345=ADVANCED_FACE('',(#1802),#14829,.T.);
#15346=ADVANCED_FACE('',(#1803),#14830,.T.);
#15347=ADVANCED_FACE('',(#1804),#14831,.T.);
#15348=ADVANCED_FACE('',(#1805),#14832,.T.);
#15349=ADVANCED_FACE('',(#1806),#14833,.T.);
#15350=ADVANCED_FACE('',(#1807),#14834,.T.);
#15351=ADVANCED_FACE('',(#1808),#1675,.T.);
#15352=ADVANCED_FACE('',(#1809),#14835,.T.);
#15353=ADVANCED_FACE('',(#1810),#1676,.T.);
#15354=ADVANCED_FACE('',(#1811),#14836,.T.);
#15355=ADVANCED_FACE('',(#1812),#14837,.F.);
#15356=ADVANCED_FACE('',(#1813),#879,.T.);
#15357=ADVANCED_FACE('',(#1814),#14838,.T.);
#15358=ADVANCED_FACE('',(#1815),#880,.T.);
#15359=ADVANCED_FACE('',(#1816),#14839,.T.);
#15360=ADVANCED_FACE('',(#1817),#14840,.T.);
#15361=ADVANCED_FACE('',(#1818),#1677,.T.);
#15362=ADVANCED_FACE('',(#1819),#14841,.T.);
#15363=ADVANCED_FACE('',(#1820),#1678,.T.);
#15364=ADVANCED_FACE('',(#1821),#14842,.T.);
#15365=ADVANCED_FACE('',(#1822),#14843,.T.);
#15366=ADVANCED_FACE('',(#1823),#1679,.T.);
#15367=ADVANCED_FACE('',(#1824),#14844,.T.);
#15368=ADVANCED_FACE('',(#1825),#1680,.T.);
#15369=ADVANCED_FACE('',(#1826),#14845,.T.);
#15370=ADVANCED_FACE('',(#1827),#14846,.T.);
#15371=ADVANCED_FACE('',(#1828),#1681,.F.);
#15372=ADVANCED_FACE('',(#1829),#14847,.T.);
#15373=ADVANCED_FACE('',(#1830),#14848,.T.);
#15374=ADVANCED_FACE('',(#1831),#14849,.T.);
#15375=ADVANCED_FACE('',(#1832),#1682,.F.);
#15376=ADVANCED_FACE('',(#1833),#14850,.T.);
#15377=ADVANCED_FACE('',(#1834),#14851,.T.);
#15378=ADVANCED_FACE('',(#1835),#1683,.T.);
#15379=ADVANCED_FACE('',(#1836),#14852,.T.);
#15380=ADVANCED_FACE('',(#1837),#1684,.T.);
#15381=ADVANCED_FACE('',(#1838),#14853,.T.);
#15382=ADVANCED_FACE('',(#1839),#14854,.T.);
#15383=ADVANCED_FACE('',(#1840),#1685,.F.);
#15384=ADVANCED_FACE('',(#1841),#14855,.T.);
#15385=ADVANCED_FACE('',(#1842),#14856,.T.);
#15386=ADVANCED_FACE('',(#1843),#14857,.T.);
#15387=ADVANCED_FACE('',(#1844),#1686,.F.);
#15388=ADVANCED_FACE('',(#1845),#14858,.T.);
#15389=ADVANCED_FACE('',(#1846,#1161),#14859,.T.);
#15390=ADVANCED_FACE('',(#1847),#491,.T.);
#15391=ADVANCED_FACE('',(#1848,#1162),#881,.T.);
#15392=ADVANCED_FACE('',(#1849),#1687,.T.);
#15393=ADVANCED_FACE('',(#1850),#1688,.T.);
#15394=ADVANCED_FACE('',(#1851),#488,.F.);
#15395=ADVANCED_FACE('',(#1852),#14860,.T.);
#15396=ADVANCED_FACE('',(#1853),#14861,.T.);
#15397=ADVANCED_FACE('',(#1854),#14862,.T.);
#15398=ADVANCED_FACE('',(#1855),#1689,.T.);
#15399=ADVANCED_FACE('',(#1856),#14863,.T.);
#15400=ADVANCED_FACE('',(#1857),#1690,.T.);
#15401=ADVANCED_FACE('',(#1858),#14864,.T.);
#15402=ADVANCED_FACE('',(#1859),#14865,.T.);
#15403=ADVANCED_FACE('',(#1860),#1691,.F.);
#15404=ADVANCED_FACE('',(#1861),#14866,.T.);
#15405=ADVANCED_FACE('',(#1862),#14867,.T.);
#15406=ADVANCED_FACE('',(#1863),#1692,.F.);
#15407=ADVANCED_FACE('',(#1864),#14868,.T.);
#15408=ADVANCED_FACE('',(#1865),#14869,.T.);
#15409=ADVANCED_FACE('',(#1866),#1693,.F.);
#15410=ADVANCED_FACE('',(#1867),#14870,.T.);
#15411=ADVANCED_FACE('',(#1868),#14871,.T.);
#15412=ADVANCED_FACE('',(#1869),#1694,.F.);
#15413=ADVANCED_FACE('',(#1870),#14872,.T.);
#15414=ADVANCED_FACE('',(#1871),#1695,.T.);
#15415=ADVANCED_FACE('',(#1872),#14873,.T.);
#15416=ADVANCED_FACE('',(#1873),#1696,.T.);
#15417=ADVANCED_FACE('',(#1874),#882,.F.);
#15418=ADVANCED_FACE('',(#1875),#14874,.F.);
#15419=ADVANCED_FACE('',(#1876),#14875,.F.);
#15420=ADVANCED_FACE('',(#1877),#883,.F.);
#15421=ADVANCED_FACE('',(#1878),#14876,.F.);
#15422=ADVANCED_FACE('',(#1879),#14877,.F.);
#15423=ADVANCED_FACE('',(#1880),#1697,.T.);
#15424=ADVANCED_FACE('',(#1881),#14878,.T.);
#15425=ADVANCED_FACE('',(#1882),#1698,.T.);
#15426=ADVANCED_FACE('',(#1883),#14879,.T.);
#15427=ADVANCED_FACE('',(#1884),#1699,.F.);
#15428=ADVANCED_FACE('',(#1885),#14880,.T.);
#15429=ADVANCED_FACE('',(#1886),#1700,.F.);
#15430=ADVANCED_FACE('',(#1887),#1701,.F.);
#15431=ADVANCED_FACE('',(#1888),#14881,.T.);
#15432=ADVANCED_FACE('',(#1889),#1702,.F.);
#15433=ADVANCED_FACE('',(#1890),#884,.T.);
#15434=ADVANCED_FACE('',(#1891),#14882,.T.);
#15435=ADVANCED_FACE('',(#1892),#885,.T.);
#15436=ADVANCED_FACE('',(#1893),#14883,.F.);
#15437=ADVANCED_FACE('',(#1894),#886,.F.);
#15438=ADVANCED_FACE('',(#1895),#14884,.F.);
#15439=ADVANCED_FACE('',(#1896),#14885,.F.);
#15440=ADVANCED_FACE('',(#1897),#887,.F.);
#16234=CLOSED_SHELL('',(#15317,#15318,#15319,#15320,#15321,#15322,#15323,
#15324,#15325,#15326,#15327,#15328,#15329,#15330,#15331,#15332,#15333,#15334,
#15335,#15336,#15337,#15338,#15339,#15340,#15341,#15342,#15343,#15344,#15345,
#15346,#15347,#15348,#15349,#15350,#15351,#15352,#15353,#15354,#15355,#15356,
#15357,#15358,#15359,#15360,#15361,#15362,#15363,#15364,#15365,#15366,#15367,
#15368,#15369,#15370,#15371,#15372,#15373,#15374,#15375,#15376,#15377,#15378,
#15379,#15380,#15381,#15382,#15383,#15384,#15385,#15386,#15387,#15388,#15389,
#15390,#15391,#15392,#15393,#15394,#15395,#15396,#15397,#15398,#15399,#15400,
#15401,#15402,#15403,#15404,#15405,#15406,#15407,#15408,#15409,#15410,#15411,
#15412,#15413,#15414,#15415,#15416,#15417,#15418,#15419,#15420,#15421,#15422,
#15423,#15424,#15425,#15426,#15427,#15428,#15429,#15430,#15431,#15432,#15433,
#15434,#15435,#15436,#15437,#15438,#15439,#15440));
#16404=AXIS2_PLACEMENT_3D('',#21834,#17807,#17808);
#16405=AXIS2_PLACEMENT_3D('',#21835,#17809,#17810);
#16406=AXIS2_PLACEMENT_3D('',#21848,#17817,#17818);
#16407=AXIS2_PLACEMENT_3D('',#21856,#17823,#17824);
#16408=AXIS2_PLACEMENT_3D('',#21864,#17829,#17830);
#16409=AXIS2_PLACEMENT_3D('',#21868,#17833,#17834);
#16410=AXIS2_PLACEMENT_3D('',#21876,#17839,#17840);
#16411=AXIS2_PLACEMENT_3D('',#21882,#17844,#17845);
#16412=AXIS2_PLACEMENT_3D('',#21895,#17852,#17853);
#16413=AXIS2_PLACEMENT_3D('',#21901,#17857,#17858);
#16414=AXIS2_PLACEMENT_3D('',#21907,#17862,#17863);
#16415=AXIS2_PLACEMENT_3D('',#21913,#17867,#17868);
#16416=AXIS2_PLACEMENT_3D('',#21926,#17875,#17876);
#16417=AXIS2_PLACEMENT_3D('',#21934,#17881,#17882);
#16418=AXIS2_PLACEMENT_3D('',#21938,#17885,#17886);
#16419=AXIS2_PLACEMENT_3D('',#21944,#17890,#17891);
#16420=AXIS2_PLACEMENT_3D('',#21957,#17898,#17899);
#16421=AXIS2_PLACEMENT_3D('',#21967,#17905,#17906);
#16422=AXIS2_PLACEMENT_3D('',#21971,#17909,#17910);
#16423=AXIS2_PLACEMENT_3D('',#21979,#17915,#17916);
#16424=AXIS2_PLACEMENT_3D('',#21985,#17920,#17921);
#16425=AXIS2_PLACEMENT_3D('',#21987,#17922,#17923);
#16426=AXIS2_PLACEMENT_3D('',#21990,#17925,#17926);
#16427=AXIS2_PLACEMENT_3D('',#21991,#17927,#17928);
#16428=AXIS2_PLACEMENT_3D('',#21994,#17930,#17931);
#16429=AXIS2_PLACEMENT_3D('',#21995,#17932,#17933);
#16430=AXIS2_PLACEMENT_3D('',#21997,#17934,#17935);
#16431=AXIS2_PLACEMENT_3D('',#21998,#17936,#17937);
#16432=AXIS2_PLACEMENT_3D('',#22001,#17939,#17940);
#16433=AXIS2_PLACEMENT_3D('',#22002,#17941,#17942);
#16434=AXIS2_PLACEMENT_3D('',#22005,#17944,#17945);
#16435=AXIS2_PLACEMENT_3D('',#22146,#17947,#17948);
#16436=AXIS2_PLACEMENT_3D('',#22172,#17950,#17951);
#16437=AXIS2_PLACEMENT_3D('',#22185,#17958,#17959);
#16438=AXIS2_PLACEMENT_3D('',#22191,#17963,#17964);
#16439=AXIS2_PLACEMENT_3D('',#22199,#17969,#17970);
#16440=AXIS2_PLACEMENT_3D('',#22205,#17974,#17975);
#16441=AXIS2_PLACEMENT_3D('',#22218,#17982,#17983);
#16442=AXIS2_PLACEMENT_3D('',#22226,#17988,#17989);
#16443=AXIS2_PLACEMENT_3D('',#22230,#17992,#17993);
#16444=AXIS2_PLACEMENT_3D('',#22236,#17997,#17998);
#16445=AXIS2_PLACEMENT_3D('',#22240,#18000,#18001);
#16446=AXIS2_PLACEMENT_3D('',#22241,#18002,#18003);
#16447=AXIS2_PLACEMENT_3D('',#22242,#18004,#18005);
#16448=AXIS2_PLACEMENT_3D('',#22248,#18009,#18010);
#16449=AXIS2_PLACEMENT_3D('',#22249,#18011,#18012);
#16450=AXIS2_PLACEMENT_3D('',#22250,#18013,#18014);
#16451=AXIS2_PLACEMENT_3D('',#22251,#18015,#18016);
#16452=AXIS2_PLACEMENT_3D('',#22259,#18021,#18022);
#16453=AXIS2_PLACEMENT_3D('',#22263,#18025,#18026);
#16454=AXIS2_PLACEMENT_3D('',#22266,#18028,#18029);
#16455=AXIS2_PLACEMENT_3D('',#22267,#18030,#18031);
#16456=AXIS2_PLACEMENT_3D('',#22271,#18034,#18035);
#16457=AXIS2_PLACEMENT_3D('',#22274,#18037,#18038);
#16458=AXIS2_PLACEMENT_3D('',#22275,#18039,#18040);
#16459=AXIS2_PLACEMENT_3D('',#22277,#18042,#18043);
#16460=AXIS2_PLACEMENT_3D('',#22285,#18048,#18049);
#16461=AXIS2_PLACEMENT_3D('',#22289,#18051,#18052);
#16462=AXIS2_PLACEMENT_3D('',#22290,#18053,#18054);
#16463=AXIS2_PLACEMENT_3D('',#22291,#18055,#18056);
#16464=AXIS2_PLACEMENT_3D('',#22297,#18060,#18061);
#16465=AXIS2_PLACEMENT_3D('',#22301,#18063,#18064);
#16466=AXIS2_PLACEMENT_3D('',#22302,#18065,#18066);
#16467=AXIS2_PLACEMENT_3D('',#22303,#18067,#18068);
#16468=AXIS2_PLACEMENT_3D('',#22308,#18072,#18073);
#16469=AXIS2_PLACEMENT_3D('',#22310,#18075,#18076);
#16470=AXIS2_PLACEMENT_3D('',#22312,#18078,#18079);
#16471=AXIS2_PLACEMENT_3D('',#22314,#18081,#18082);
#16472=AXIS2_PLACEMENT_3D('',#22316,#18084,#18085);
#16473=AXIS2_PLACEMENT_3D('',#22317,#18086,#18087);
#16474=AXIS2_PLACEMENT_3D('',#22321,#18090,#18091);
#16475=AXIS2_PLACEMENT_3D('',#22324,#18093,#18094);
#16476=AXIS2_PLACEMENT_3D('',#22325,#18095,#18096);
#16477=AXIS2_PLACEMENT_3D('',#22326,#18097,#18098);
#16478=AXIS2_PLACEMENT_3D('',#22330,#18101,#18102);
#16479=AXIS2_PLACEMENT_3D('',#22334,#18105,#18106);
#16480=AXIS2_PLACEMENT_3D('',#22338,#18109,#18110);
#16481=AXIS2_PLACEMENT_3D('',#22341,#18112,#18113);
#16482=AXIS2_PLACEMENT_3D('',#22342,#18114,#18115);
#16483=AXIS2_PLACEMENT_3D('',#22343,#18116,#18117);
#16484=AXIS2_PLACEMENT_3D('',#22347,#18120,#18121);
#16485=AXIS2_PLACEMENT_3D('',#22351,#18124,#18125);
#16486=AXIS2_PLACEMENT_3D('',#22355,#18127,#18128);
#16487=AXIS2_PLACEMENT_3D('',#22356,#18129,#18130);
#16488=AXIS2_PLACEMENT_3D('',#22357,#18131,#18132);
#16489=AXIS2_PLACEMENT_3D('',#22363,#18136,#18137);
#16490=AXIS2_PLACEMENT_3D('',#22366,#18139,#18140);
#16491=AXIS2_PLACEMENT_3D('',#22367,#18141,#18142);
#16492=AXIS2_PLACEMENT_3D('',#22368,#18143,#18144);
#16493=AXIS2_PLACEMENT_3D('',#22372,#18147,#18148);
#16494=AXIS2_PLACEMENT_3D('',#22378,#18152,#18153);
#16495=AXIS2_PLACEMENT_3D('',#22382,#18155,#18156);
#16496=AXIS2_PLACEMENT_3D('',#22383,#18157,#18158);
#16497=AXIS2_PLACEMENT_3D('',#22384,#18159,#18160);
#16498=AXIS2_PLACEMENT_3D('',#22389,#18164,#18165);
#16499=AXIS2_PLACEMENT_3D('',#22393,#18168,#18169);
#16500=AXIS2_PLACEMENT_3D('',#22399,#18173,#18174);
#16501=AXIS2_PLACEMENT_3D('',#22402,#18176,#18177);
#16502=AXIS2_PLACEMENT_3D('',#22403,#18178,#18179);
#16503=AXIS2_PLACEMENT_3D('',#22404,#18180,#18181);
#16504=AXIS2_PLACEMENT_3D('',#22406,#18183,#18184);
#16505=AXIS2_PLACEMENT_3D('',#22408,#18185,#18186);
#16506=AXIS2_PLACEMENT_3D('',#22501,#18188,#18189);
#16507=AXIS2_PLACEMENT_3D('',#22503,#18190,#18191);
#16508=AXIS2_PLACEMENT_3D('',#22507,#18193,#18194);
#16509=AXIS2_PLACEMENT_3D('',#22508,#18195,#18196);
#16510=AXIS2_PLACEMENT_3D('',#22509,#18197,#18198);
#16511=AXIS2_PLACEMENT_3D('',#22511,#18199,#18200);
#16512=AXIS2_PLACEMENT_3D('',#22513,#18202,#18203);
#16513=AXIS2_PLACEMENT_3D('',#22515,#18205,#18206);
#16514=AXIS2_PLACEMENT_3D('',#22516,#18207,#18208);
#16515=AXIS2_PLACEMENT_3D('',#22517,#18209,#18210);
#16516=AXIS2_PLACEMENT_3D('',#22518,#18211,#18212);
#16517=AXIS2_PLACEMENT_3D('',#22524,#18216,#18217);
#16518=AXIS2_PLACEMENT_3D('',#22530,#18221,#18222);
#16519=AXIS2_PLACEMENT_3D('',#22534,#18224,#18225);
#16520=AXIS2_PLACEMENT_3D('',#22535,#18226,#18227);
#16521=AXIS2_PLACEMENT_3D('',#22536,#18228,#18229);
#16522=AXIS2_PLACEMENT_3D('',#22542,#18233,#18234);
#16523=AXIS2_PLACEMENT_3D('',#22545,#18236,#18237);
#16524=AXIS2_PLACEMENT_3D('',#22546,#18238,#18239);
#16525=AXIS2_PLACEMENT_3D('',#22547,#18240,#18241);
#16526=AXIS2_PLACEMENT_3D('',#22551,#18244,#18245);
#16527=AXIS2_PLACEMENT_3D('',#22557,#18249,#18250);
#16528=AXIS2_PLACEMENT_3D('',#22561,#18252,#18253);
#16529=AXIS2_PLACEMENT_3D('',#22562,#18254,#18255);
#16530=AXIS2_PLACEMENT_3D('',#22563,#18256,#18257);
#16531=AXIS2_PLACEMENT_3D('',#22566,#18260,#18261);
#16532=AXIS2_PLACEMENT_3D('',#22572,#18265,#18266);
#16533=AXIS2_PLACEMENT_3D('',#22576,#18268,#18269);
#16534=AXIS2_PLACEMENT_3D('',#22577,#18270,#18271);
#16535=AXIS2_PLACEMENT_3D('',#22578,#18272,#18273);
#16536=AXIS2_PLACEMENT_3D('',#22581,#18276,#18277);
#16537=AXIS2_PLACEMENT_3D('',#22587,#18281,#18282);
#16538=AXIS2_PLACEMENT_3D('',#22590,#18284,#18285);
#16539=AXIS2_PLACEMENT_3D('',#22591,#18286,#18287);
#16540=AXIS2_PLACEMENT_3D('',#22592,#18288,#18289);
#16541=AXIS2_PLACEMENT_3D('',#22594,#18291,#18292);
#16542=AXIS2_PLACEMENT_3D('',#22598,#18295,#18296);
#16543=AXIS2_PLACEMENT_3D('',#22602,#18298,#18299);
#16544=AXIS2_PLACEMENT_3D('',#22603,#18300,#18301);
#16545=AXIS2_PLACEMENT_3D('',#22604,#18302,#18303);
#16546=AXIS2_PLACEMENT_3D('',#22607,#18306,#18307);
#16547=AXIS2_PLACEMENT_3D('',#22610,#18309,#18310);
#16548=AXIS2_PLACEMENT_3D('',#22611,#18311,#18312);
#16549=AXIS2_PLACEMENT_3D('',#22615,#18315,#18316);
#16550=AXIS2_PLACEMENT_3D('',#22616,#18317,#18318);
#16551=AXIS2_PLACEMENT_3D('',#22617,#18319,#18320);
#16552=AXIS2_PLACEMENT_3D('',#22620,#18322,#18323);
#16553=AXIS2_PLACEMENT_3D('',#22621,#18324,#18325);
#16554=AXIS2_PLACEMENT_3D('',#22623,#18327,#18328);
#16555=AXIS2_PLACEMENT_3D('',#22627,#18331,#18332);
#16556=AXIS2_PLACEMENT_3D('',#22630,#18334,#18335);
#16557=AXIS2_PLACEMENT_3D('',#22631,#18336,#18337);
#16558=AXIS2_PLACEMENT_3D('',#22633,#18339,#18340);
#16559=AXIS2_PLACEMENT_3D('',#22634,#18341,#18342);
#16560=AXIS2_PLACEMENT_3D('',#22636,#18343,#18344);
#16561=AXIS2_PLACEMENT_3D('',#22638,#18346,#18347);
#16562=AXIS2_PLACEMENT_3D('',#22642,#18350,#18351);
#16563=AXIS2_PLACEMENT_3D('',#22643,#18352,#18353);
#16564=AXIS2_PLACEMENT_3D('',#22644,#18354,#18355);
#16565=AXIS2_PLACEMENT_3D('',#22646,#18357,#18358);
#16566=AXIS2_PLACEMENT_3D('',#22648,#18360,#18361);
#16567=AXIS2_PLACEMENT_3D('',#22649,#18362,#18363);
#16568=AXIS2_PLACEMENT_3D('',#22650,#18364,#18365);
#16569=AXIS2_PLACEMENT_3D('',#22651,#18366,#18367);
#16570=AXIS2_PLACEMENT_3D('',#22653,#18369,#18370);
#16571=AXIS2_PLACEMENT_3D('',#22654,#18371,#18372);
#16572=AXIS2_PLACEMENT_3D('',#22655,#18373,#18374);
#16573=AXIS2_PLACEMENT_3D('',#22656,#18375,#18376);
#16574=AXIS2_PLACEMENT_3D('',#22658,#18378,#18379);
#16575=AXIS2_PLACEMENT_3D('',#22660,#18381,#18382);
#16576=AXIS2_PLACEMENT_3D('',#22661,#18383,#18384);
#16577=AXIS2_PLACEMENT_3D('',#22663,#18386,#18387);
#16578=AXIS2_PLACEMENT_3D('',#22664,#18388,#18389);
#16579=AXIS2_PLACEMENT_3D('',#22666,#18391,#18392);
#16580=AXIS2_PLACEMENT_3D('',#22668,#18394,#18395);
#17807=DIRECTION('axis',(0.,0.,1.));
#17808=DIRECTION('refdir',(1.,0.,0.));
#17809=DIRECTION('center_axis',(0.707106781186553,-0.707106781186542,0.));
#17810=DIRECTION('ref_axis',(0.,0.,-1.));
#17811=DIRECTION('',(0.577350269189623,0.577350269189632,0.577350269189623));
#17812=DIRECTION('',(0.,0.,1.));
#17813=DIRECTION('',(-0.577350269189623,-0.577350269189632,0.577350269189623));
#17814=DIRECTION('',(-0.57735026918962,-0.577350269189629,-0.577350269189629));
#17815=DIRECTION('',(0.,0.,-1.));
#17816=DIRECTION('',(0.57735026918962,0.577350269189629,-0.577350269189629));
#17817=DIRECTION('center_axis',(0.,-0.707106781186548,0.707106781186548));
#17818=DIRECTION('ref_axis',(1.,0.,0.));
#17819=DIRECTION('',(0.577350269189629,-0.577350269189623,-0.577350269189625));
#17820=DIRECTION('',(1.,0.,0.));
#17821=DIRECTION('',(0.,0.707106781186548,0.707106781186548));
#17822=DIRECTION('',(1.,0.,0.));
#17823=DIRECTION('center_axis',(0.707106781186548,0.,0.707106781186548));
#17824=DIRECTION('ref_axis',(0.707106781186548,0.,-0.707106781186548));
#17825=DIRECTION('',(0.,1.,0.));
#17826=DIRECTION('',(0.577350269189619,-0.57735026918964,-0.577350269189619));
#17827=DIRECTION('',(0.577350269189627,0.577350269189623,-0.577350269189627));
#17828=DIRECTION('',(0.,1.,0.));
#17829=DIRECTION('center_axis',(1.,0.,0.));
#17830=DIRECTION('ref_axis',(0.,1.,0.));
#17831=DIRECTION('',(0.,-1.,0.));
#17832=DIRECTION('',(0.,0.,-1.));
#17833=DIRECTION('center_axis',(0.707106781186561,0.707106781186534,0.));
#17834=DIRECTION('ref_axis',(0.,0.,-1.));
#17835=DIRECTION('',(-0.577350269189619,0.57735026918964,-0.577350269189618));
#17836=DIRECTION('',(-0.577350269189612,0.577350269189633,0.577350269189633));
#17837=DIRECTION('',(0.,0.,1.));
#17838=DIRECTION('',(0.577350269189612,-0.577350269189633,0.577350269189633));
#17839=DIRECTION('center_axis',(0.,0.707106781186548,0.707106781186548));
#17840=DIRECTION('ref_axis',(1.,0.,0.));
#17841=DIRECTION('',(-1.,0.,0.));
#17842=DIRECTION('',(0.,-0.707106781186548,0.707106781186548));
#17843=DIRECTION('',(-1.,0.,0.));
#17844=DIRECTION('center_axis',(0.707106781186558,0.707106781186537,0.));
#17845=DIRECTION('ref_axis',(0.,0.,-1.));
#17846=DIRECTION('',(0.57735026918962,-0.577350269189637,-0.57735026918962));
#17847=DIRECTION('',(0.,0.,-1.));
#17848=DIRECTION('',(-0.57735026918962,0.577350269189637,-0.57735026918962));
#17849=DIRECTION('',(-0.577350269189614,0.577350269189632,0.577350269189632));
#17850=DIRECTION('',(0.,0.,1.));
#17851=DIRECTION('',(0.577350269189614,-0.577350269189632,0.577350269189632));
#17852=DIRECTION('center_axis',(1.,0.,0.));
#17853=DIRECTION('ref_axis',(0.,1.,0.));
#17854=DIRECTION('',(0.,1.,0.));
#17855=DIRECTION('',(0.,0.,1.));
#17856=DIRECTION('',(0.,-1.,0.));
#17857=DIRECTION('center_axis',(0.707106781186548,0.,0.707106781186548));
#17858=DIRECTION('ref_axis',(0.707106781186548,0.,-0.707106781186548));
#17859=DIRECTION('',(0.577350269189627,0.577350269189624,-0.577350269189627));
#17860=DIRECTION('',(0.,1.,0.));
#17861=DIRECTION('',(-0.70710678118655,0.,0.707106781186545));
#17862=DIRECTION('center_axis',(0.,0.707106781186548,0.707106781186548));
#17863=DIRECTION('ref_axis',(1.,0.,0.));
#17864=DIRECTION('',(-1.,0.,0.));
#17865=DIRECTION('',(0.,-0.707106781186548,0.707106781186548));
#17866=DIRECTION('',(-1.,0.,0.));
#17867=DIRECTION('center_axis',(-0.707106781186555,0.70710678118654,0.));
#17868=DIRECTION('ref_axis',(0.,0.,1.));
#17869=DIRECTION('',(-0.577350269189622,-0.577350269189635,0.577350269189621));
#17870=DIRECTION('',(0.,0.,1.));
#17871=DIRECTION('',(0.577350269189622,0.577350269189634,0.577350269189622));
#17872=DIRECTION('',(0.577350269189617,0.57735026918963,-0.57735026918963));
#17873=DIRECTION('',(0.,0.,-1.));
#17874=DIRECTION('',(-0.577350269189617,-0.57735026918963,-0.57735026918963));
#17875=DIRECTION('center_axis',(-0.707106781186548,0.,0.707106781186548));
#17876=DIRECTION('ref_axis',(0.707106781186548,0.,0.707106781186548));
#17877=DIRECTION('',(0.,-1.,0.));
#17878=DIRECTION('',(0.707106781186548,0.,0.707106781186548));
#17879=DIRECTION('',(0.,-1.,0.));
#17880=DIRECTION('',(-0.577350269189629,0.577350269189623,-0.577350269189625));
#17881=DIRECTION('center_axis',(-1.,0.,0.));
#17882=DIRECTION('ref_axis',(0.,-1.,0.));
#17883=DIRECTION('',(0.,1.,0.));
#17884=DIRECTION('',(0.,0.,-1.));
#17885=DIRECTION('center_axis',(-0.707106781186547,0.,-0.707106781186548));
#17886=DIRECTION('ref_axis',(-0.707106781186548,0.,0.707106781186547));
#17887=DIRECTION('',(0.577350269189627,-0.577350269189624,-0.577350269189627));
#17888=DIRECTION('',(0.,-1.,0.));
#17889=DIRECTION('',(-0.707106781186548,0.,0.707106781186547));
#17890=DIRECTION('center_axis',(-0.707106781186561,-0.707106781186534,0.));
#17891=DIRECTION('ref_axis',(0.,0.,1.));
#17892=DIRECTION('',(-0.577350269189619,0.57735026918964,-0.577350269189619));
#17893=DIRECTION('',(0.,0.,-1.));
#17894=DIRECTION('',(0.577350269189619,-0.57735026918964,-0.577350269189618));
#17895=DIRECTION('',(0.577350269189612,-0.577350269189633,0.577350269189633));
#17896=DIRECTION('',(0.,0.,1.));
#17897=DIRECTION('',(-0.577350269189612,0.577350269189633,0.577350269189633));
#17898=DIRECTION('center_axis',(-0.707106781186547,0.,-0.707106781186548));
#17899=DIRECTION('ref_axis',(-0.707106781186548,0.,0.707106781186547));
#17900=DIRECTION('',(0.,1.,0.));
#17901=DIRECTION('',(-0.577350269189623,-0.577350269189632,0.577350269189623));
#17902=DIRECTION('',(0.577350269189627,-0.577350269189624,-0.577350269189627));
#17903=DIRECTION('',(0.,-1.,0.));
#17904=DIRECTION('',(-0.577350269189627,-0.577350269189624,0.577350269189627));
#17905=DIRECTION('center_axis',(-1.,0.,0.));
#17906=DIRECTION('ref_axis',(0.,-1.,0.));
#17907=DIRECTION('',(0.,-1.,0.));
#17908=DIRECTION('',(0.,0.,1.));
#17909=DIRECTION('center_axis',(-0.707106781186548,0.,0.707106781186548));
#17910=DIRECTION('ref_axis',(0.707106781186548,0.,0.707106781186548));
#17911=DIRECTION('',(-0.577350269189627,-0.577350269189623,-0.577350269189627));
#17912=DIRECTION('',(0.,-1.,0.));
#17913=DIRECTION('',(-0.577350269189629,0.577350269189623,-0.577350269189625));
#17914=DIRECTION('',(0.577350269189623,0.577350269189632,0.577350269189623));
#17915=DIRECTION('center_axis',(-0.707106781186553,0.707106781186542,0.));
#17916=DIRECTION('ref_axis',(0.,0.,1.));
#17917=DIRECTION('',(0.57735026918962,0.577350269189629,-0.577350269189629));
#17918=DIRECTION('',(0.,0.,-1.));
#17919=DIRECTION('',(-0.57735026918962,-0.577350269189629,-0.577350269189629));
#17920=DIRECTION('center_axis',(0.,2.96961385686688E-15,1.));
#17921=DIRECTION('ref_axis',(1.,2.98726371833858E-17,0.));
#17922=DIRECTION('center_axis',(0.,0.,-1.));
#17923=DIRECTION('ref_axis',(1.,6.12323399573676E-17,0.));
#17924=DIRECTION('',(-0.923879532511288,1.22196591669764E-15,0.382683432365087));
#17925=DIRECTION('center_axis',(0.,0.,1.));
#17926=DIRECTION('ref_axis',(1.,0.,0.));
#17927=DIRECTION('center_axis',(0.,0.,1.));
#17928=DIRECTION('ref_axis',(1.,0.,0.));
#17929=DIRECTION('',(0.707106781186547,8.65956056235493E-17,-0.707106781186547));
#17930=DIRECTION('center_axis',(0.,0.,1.));
#17931=DIRECTION('ref_axis',(1.,6.12323399573677E-17,0.));
#17932=DIRECTION('center_axis',(0.,0.,1.));
#17933=DIRECTION('ref_axis',(1.,0.,0.));
#17934=DIRECTION('center_axis',(0.,0.,-1.));
#17935=DIRECTION('ref_axis',(1.,0.,0.));
#17936=DIRECTION('center_axis',(0.,-1.22099907537238E-15,1.));
#17937=DIRECTION('ref_axis',(1.,3.09374953297515E-17,0.));
#17938=DIRECTION('',(0.382683432365087,1.18676052590658E-15,-0.923879532511288));
#17939=DIRECTION('center_axis',(0.,0.,-1.));
#17940=DIRECTION('ref_axis',(1.,0.,0.));
#17941=DIRECTION('center_axis',(0.,0.,-1.));
#17942=DIRECTION('ref_axis',(1.,0.,0.));
#17943=DIRECTION('',(0.,0.,-1.));
#17944=DIRECTION('center_axis',(0.,0.,-1.));
#17945=DIRECTION('ref_axis',(1.,0.,0.));
#17946=DIRECTION('',(-0.62463654800244,0.780915605491141,4.73897997350133E-15));
#17947=DIRECTION('center_axis',(0.,1.,0.));
#17948=DIRECTION('ref_axis',(0.,0.,1.));
#17949=DIRECTION('',(0.,1.,0.));
#17950=DIRECTION('center_axis',(0.707106781186555,-0.70710678118654,0.));
#17951=DIRECTION('ref_axis',(0.,0.,-1.));
#17952=DIRECTION('',(0.577350269189622,0.577350269189635,0.577350269189621));
#17953=DIRECTION('',(0.,0.,1.));
#17954=DIRECTION('',(-0.357406744336599,-0.357406744336607,0.862856209461009));
#17955=DIRECTION('',(-0.577350269189617,-0.57735026918963,-0.57735026918963));
#17956=DIRECTION('',(0.,0.,-1.));
#17957=DIRECTION('',(0.577350269189617,0.57735026918963,-0.57735026918963));
#17958=DIRECTION('center_axis',(0.,1.,0.));
#17959=DIRECTION('ref_axis',(1.,0.,0.));
#17960=DIRECTION('',(1.,0.,0.));
#17961=DIRECTION('',(0.,0.,-1.));
#17962=DIRECTION('',(-1.,0.,0.));
#17963=DIRECTION('center_axis',(0.,-0.707106781186548,0.707106781186548));
#17964=DIRECTION('ref_axis',(1.,0.,0.));
#17965=DIRECTION('',(0.281084637714827,-0.678598344545846,-0.678598344545846));
#17966=DIRECTION('',(0.577350269189629,-0.577350269189623,-0.577350269189625));
#17967=DIRECTION('',(1.,0.,0.));
#17968=DIRECTION('',(0.,0.707106781186548,0.707106781186548));
#17969=DIRECTION('center_axis',(0.923879532511283,0.,0.382683432365098));
#17970=DIRECTION('ref_axis',(0.382683432365098,0.,-0.923879532511283));
#17971=DIRECTION('',(0.,1.,0.));
#17972=DIRECTION('',(-0.38268343236509,0.,0.923879532511287));
#17973=DIRECTION('',(0.,-1.,0.));
#17974=DIRECTION('center_axis',(-0.707106781186558,-0.707106781186537,0.));
#17975=DIRECTION('ref_axis',(0.,0.,1.));
#17976=DIRECTION('',(-0.357406744336599,0.357406744336609,-0.862856209461008));
#17977=DIRECTION('',(0.,0.,-1.));
#17978=DIRECTION('',(0.57735026918962,-0.577350269189637,-0.57735026918962));
#17979=DIRECTION('',(0.577350269189614,-0.577350269189632,0.577350269189632));
#17980=DIRECTION('',(0.,0.,1.));
#17981=DIRECTION('',(-0.577350269189614,0.577350269189632,0.577350269189632));
#17982=DIRECTION('center_axis',(-0.707106781186547,0.,-0.707106781186548));
#17983=DIRECTION('ref_axis',(-0.707106781186548,0.,0.707106781186547));
#17984=DIRECTION('',(0.,1.,0.));
#17985=DIRECTION('',(-0.707106781186556,0.,0.707106781186539));
#17986=DIRECTION('',(0.,-1.,0.));
#17987=DIRECTION('',(-0.577350269189627,-0.577350269189624,0.577350269189627));
#17988=DIRECTION('center_axis',(-1.,0.,0.));
#17989=DIRECTION('ref_axis',(0.,-1.,0.));
#17990=DIRECTION('',(0.,-1.,0.));
#17991=DIRECTION('',(0.,0.,1.));
#17992=DIRECTION('center_axis',(-0.923879532511283,0.,0.382683432365098));
#17993=DIRECTION('ref_axis',(0.382683432365098,0.,0.923879532511283));
#17994=DIRECTION('',(0.281084637714827,0.678598344545846,0.678598344545846));
#17995=DIRECTION('',(0.,1.,0.));
#17996=DIRECTION('',(0.382683432365096,0.,0.923879532511284));
#17997=DIRECTION('center_axis',(0.,0.,-1.));
#17998=DIRECTION('ref_axis',(0.707106781186548,0.707106781186548,0.));
#17999=DIRECTION('',(0.,-0.382683432365096,0.923879532511284));
#18000=DIRECTION('center_axis',(0.,0.,-1.));
#18001=DIRECTION('ref_axis',(0.707106781186548,0.707106781186548,0.));
#18002=DIRECTION('center_axis',(0.,0.,1.));
#18003=DIRECTION('ref_axis',(0.707106781186548,0.707106781186548,0.));
#18004=DIRECTION('center_axis',(0.,0.923879532511283,0.382683432365098));
#18005=DIRECTION('ref_axis',(0.,-0.382683432365098,0.923879532511283));
#18006=DIRECTION('',(0.,-0.38268343236509,0.923879532511287));
#18007=DIRECTION('',(1.,0.,0.));
#18008=DIRECTION('',(-1.,0.,0.));
#18009=DIRECTION('center_axis',(0.,0.,-1.));
#18010=DIRECTION('ref_axis',(-0.707106781186548,0.707106781186548,0.));
#18011=DIRECTION('center_axis',(0.,0.,-1.));
#18012=DIRECTION('ref_axis',(-0.707106781186548,0.707106781186548,0.));
#18013=DIRECTION('center_axis',(0.,0.,1.));
#18014=DIRECTION('ref_axis',(-0.707106781186548,0.707106781186548,0.));
#18015=DIRECTION('center_axis',(0.,-0.707106781186548,0.707106781186548));
#18016=DIRECTION('ref_axis',(1.,0.,0.));
#18017=DIRECTION('',(1.,0.,0.));
#18018=DIRECTION('',(0.,0.707106781186548,0.707106781186548));
#18019=DIRECTION('',(1.,0.,0.));
#18020=DIRECTION('',(-0.577350269189627,-0.577350269189624,-0.577350269189627));
#18021=DIRECTION('center_axis',(0.,1.,0.));
#18022=DIRECTION('ref_axis',(1.,0.,0.));
#18023=DIRECTION('',(-1.,0.,0.));
#18024=DIRECTION('',(0.,0.,-1.));
#18025=DIRECTION('center_axis',(0.,0.,1.));
#18026=DIRECTION('ref_axis',(-0.707106781186547,0.707106781186547,0.));
#18027=DIRECTION('',(0.,0.,-1.));
#18028=DIRECTION('center_axis',(0.,0.,-1.));
#18029=DIRECTION('ref_axis',(-0.707106781186548,0.707106781186548,0.));
#18030=DIRECTION('center_axis',(0.,1.,0.));
#18031=DIRECTION('ref_axis',(-1.,0.,0.));
#18032=DIRECTION('',(0.,0.,1.));
#18033=DIRECTION('',(1.,0.,0.));
#18034=DIRECTION('center_axis',(0.,0.,1.));
#18035=DIRECTION('ref_axis',(0.707106781186547,0.707106781186547,0.));
#18036=DIRECTION('',(0.,0.,-1.));
#18037=DIRECTION('center_axis',(0.,0.,-1.));
#18038=DIRECTION('ref_axis',(0.707106781186548,0.707106781186548,0.));
#18039=DIRECTION('center_axis',(1.,0.,0.));
#18040=DIRECTION('ref_axis',(0.,1.,0.));
#18041=DIRECTION('',(0.,-1.,0.));
#18042=DIRECTION('center_axis',(-0.382683432365098,0.,0.923879532511283));
#18043=DIRECTION('ref_axis',(0.923879532511283,0.,0.382683432365098));
#18044=DIRECTION('',(0.678598344545834,0.678598344545859,0.281084637714822));
#18045=DIRECTION('',(0.,1.,0.));
#18046=DIRECTION('',(-0.923879532511283,0.,-0.382683432365098));
#18047=DIRECTION('',(0.,-1.,0.));
#18048=DIRECTION('center_axis',(0.,0.,-1.));
#18049=DIRECTION('ref_axis',(-0.707106781186548,0.707106781186548,0.));
#18050=DIRECTION('',(0.,0.923879532511291,-0.38268343236508));
#18051=DIRECTION('center_axis',(0.,0.,1.));
#18052=DIRECTION('ref_axis',(-0.707106781186548,0.707106781186548,0.));
#18053=DIRECTION('center_axis',(0.,0.,-1.));
#18054=DIRECTION('ref_axis',(-0.707106781186548,0.707106781186548,0.));
#18055=DIRECTION('center_axis',(0.,0.382683432365103,0.923879532511281));
#18056=DIRECTION('ref_axis',(1.,0.,0.));
#18057=DIRECTION('',(0.,0.923879532511281,-0.382683432365103));
#18058=DIRECTION('',(-1.,0.,0.));
#18059=DIRECTION('',(1.,0.,0.));
#18060=DIRECTION('center_axis',(0.,0.,-1.));
#18061=DIRECTION('ref_axis',(0.707106781186548,0.707106781186548,0.));
#18062=DIRECTION('',(0.923879532511291,0.,-0.38268343236508));
#18063=DIRECTION('center_axis',(0.,0.,1.));
#18064=DIRECTION('ref_axis',(0.707106781186548,0.707106781186548,0.));
#18065=DIRECTION('center_axis',(0.,0.,-1.));
#18066=DIRECTION('ref_axis',(0.707106781186548,0.707106781186548,0.));
#18067=DIRECTION('center_axis',(0.382683432365098,0.,0.923879532511283));
#18068=DIRECTION('ref_axis',(0.923879532511283,0.,-0.382683432365098));
#18069=DIRECTION('',(0.678598344545834,-0.678598344545859,-0.281084637714822));
#18070=DIRECTION('',(0.,1.,0.));
#18071=DIRECTION('',(0.,-1.,0.));
#18072=DIRECTION('center_axis',(-0.707106781186548,0.,0.707106781186548));
#18073=DIRECTION('ref_axis',(0.707106781186548,0.,0.707106781186548));
#18074=DIRECTION('',(0.70710678118655,0.,0.707106781186545));
#18075=DIRECTION('center_axis',(0.,0.,-1.));
#18076=DIRECTION('ref_axis',(-0.707106781186547,0.707106781186547,0.));
#18077=DIRECTION('',(0.,-0.707106781186548,0.707106781186548));
#18078=DIRECTION('center_axis',(0.,0.707106781186548,0.707106781186548));
#18079=DIRECTION('ref_axis',(1.,0.,0.));
#18080=DIRECTION('',(0.,-0.70710678118655,0.707106781186545));
#18081=DIRECTION('center_axis',(0.,0.,-1.));
#18082=DIRECTION('ref_axis',(0.707106781186547,0.707106781186547,0.));
#18083=DIRECTION('',(-0.707106781186548,0.,0.707106781186548));
#18084=DIRECTION('center_axis',(0.707106781186548,0.,0.707106781186548));
#18085=DIRECTION('ref_axis',(0.707106781186548,0.,-0.707106781186548));
#18086=DIRECTION('center_axis',(0.,-0.382683432365086,0.923879532511289));
#18087=DIRECTION('ref_axis',(1.,0.,0.));
#18088=DIRECTION('',(-1.,0.,0.));
#18089=DIRECTION('',(0.,-0.923879532511289,-0.382683432365086));
#18090=DIRECTION('center_axis',(0.,0.,1.));
#18091=DIRECTION('ref_axis',(0.,1.,0.));
#18092=DIRECTION('',(0.,0.923879532511287,-0.38268343236509));
#18093=DIRECTION('center_axis',(0.,0.,-1.));
#18094=DIRECTION('ref_axis',(0.,1.,0.));
#18095=DIRECTION('center_axis',(0.,0.,1.));
#18096=DIRECTION('ref_axis',(0.,1.,0.));
#18097=DIRECTION('center_axis',(0.,0.382683432365089,0.923879532511287));
#18098=DIRECTION('ref_axis',(1.,0.,0.));
#18099=DIRECTION('',(1.,0.,0.));
#18100=DIRECTION('',(0.678598344545841,0.678598344545853,-0.281084637714822));
#18101=DIRECTION('center_axis',(0.382683432365098,0.,0.923879532511283));
#18102=DIRECTION('ref_axis',(0.923879532511283,0.,-0.382683432365098));
#18103=DIRECTION('',(0.,-1.,0.));
#18104=DIRECTION('',(0.678598344545841,-0.678598344545852,-0.281084637714823));
#18105=DIRECTION('center_axis',(0.,-0.382683432365089,0.923879532511287));
#18106=DIRECTION('ref_axis',(1.,0.,0.));
#18107=DIRECTION('',(-1.,0.,0.));
#18108=DIRECTION('',(0.,-0.923879532511287,-0.38268343236509));
#18109=DIRECTION('center_axis',(0.,0.,1.));
#18110=DIRECTION('ref_axis',(0.,1.,0.));
#18111=DIRECTION('',(0.,0.923879532511287,-0.38268343236509));
#18112=DIRECTION('center_axis',(0.,0.,-1.));
#18113=DIRECTION('ref_axis',(0.,1.,0.));
#18114=DIRECTION('center_axis',(0.,0.,1.));
#18115=DIRECTION('ref_axis',(0.,1.,0.));
#18116=DIRECTION('center_axis',(0.,0.382683432365086,0.923879532511289));
#18117=DIRECTION('ref_axis',(1.,0.,0.));
#18118=DIRECTION('',(1.,0.,0.));
#18119=DIRECTION('',(0.67859834454584,0.678598344545855,-0.28108463771482));
#18120=DIRECTION('center_axis',(0.382683432365098,0.,0.923879532511283));
#18121=DIRECTION('ref_axis',(0.923879532511283,0.,-0.382683432365098));
#18122=DIRECTION('',(0.,-1.,0.));
#18123=DIRECTION('',(0.923879532511283,0.,-0.382683432365098));
#18124=DIRECTION('center_axis',(0.,0.,-1.));
#18125=DIRECTION('ref_axis',(0.707106781186548,-0.707106781186548,0.));
#18126=DIRECTION('',(0.,-0.923879532511291,-0.38268343236508));
#18127=DIRECTION('center_axis',(0.,0.,1.));
#18128=DIRECTION('ref_axis',(0.707106781186548,-0.707106781186548,0.));
#18129=DIRECTION('center_axis',(0.,0.,-1.));
#18130=DIRECTION('ref_axis',(0.707106781186548,-0.707106781186548,0.));
#18131=DIRECTION('center_axis',(0.,-0.382683432365103,0.923879532511281));
#18132=DIRECTION('ref_axis',(1.,0.,0.));
#18133=DIRECTION('',(0.,-0.923879532511281,-0.382683432365103));
#18134=DIRECTION('',(1.,0.,0.));
#18135=DIRECTION('',(-1.,0.,0.));
#18136=DIRECTION('center_axis',(0.,0.,-1.));
#18137=DIRECTION('ref_axis',(-0.707106781186548,-0.707106781186548,0.));
#18138=DIRECTION('',(-0.923879532511291,0.,-0.38268343236508));
#18139=DIRECTION('center_axis',(0.,0.,1.));
#18140=DIRECTION('ref_axis',(-0.707106781186548,-0.707106781186548,0.));
#18141=DIRECTION('center_axis',(0.,0.,-1.));
#18142=DIRECTION('ref_axis',(-0.707106781186548,-0.707106781186548,0.));
#18143=DIRECTION('center_axis',(-0.382683432365098,0.,0.923879532511283));
#18144=DIRECTION('ref_axis',(0.923879532511283,0.,0.382683432365098));
#18145=DIRECTION('',(0.,1.,0.));
#18146=DIRECTION('',(-0.678598344545837,0.678598344545857,-0.281084637714821));
#18147=DIRECTION('center_axis',(0.,0.382683432365086,0.923879532511289));
#18148=DIRECTION('ref_axis',(1.,0.,0.));
#18149=DIRECTION('',(1.,0.,0.));
#18150=DIRECTION('',(0.,0.923879532511289,-0.382683432365086));
#18151=DIRECTION('',(-1.,0.,0.));
#18152=DIRECTION('center_axis',(0.,0.,1.));
#18153=DIRECTION('ref_axis',(0.,-1.,0.));
#18154=DIRECTION('',(0.,-0.923879532511287,-0.38268343236509));
#18155=DIRECTION('center_axis',(0.,0.,-1.));
#18156=DIRECTION('ref_axis',(0.,-1.,0.));
#18157=DIRECTION('center_axis',(0.,0.,1.));
#18158=DIRECTION('ref_axis',(0.,-1.,0.));
#18159=DIRECTION('center_axis',(0.,-0.382683432365089,0.923879532511287));
#18160=DIRECTION('ref_axis',(1.,0.,0.));
#18161=DIRECTION('',(1.,0.,0.));
#18162=DIRECTION('',(-1.,0.,0.));
#18163=DIRECTION('',(-0.678598344545841,-0.678598344545853,-0.281084637714822));
#18164=DIRECTION('center_axis',(-0.382683432365098,0.,0.923879532511283));
#18165=DIRECTION('ref_axis',(0.923879532511283,0.,0.382683432365098));
#18166=DIRECTION('',(0.,1.,0.));
#18167=DIRECTION('',(-0.678598344545841,0.678598344545852,-0.281084637714823));
#18168=DIRECTION('center_axis',(0.,0.382683432365089,0.923879532511287));
#18169=DIRECTION('ref_axis',(1.,0.,0.));
#18170=DIRECTION('',(1.,0.,0.));
#18171=DIRECTION('',(0.,0.923879532511287,-0.38268343236509));
#18172=DIRECTION('',(-1.,0.,0.));
#18173=DIRECTION('center_axis',(0.,0.,1.));
#18174=DIRECTION('ref_axis',(0.,-1.,0.));
#18175=DIRECTION('',(0.,-0.923879532511287,-0.38268343236509));
#18176=DIRECTION('center_axis',(0.,0.,-1.));
#18177=DIRECTION('ref_axis',(0.,-1.,0.));
#18178=DIRECTION('center_axis',(0.,0.,1.));
#18179=DIRECTION('ref_axis',(0.,-1.,0.));
#18180=DIRECTION('center_axis',(0.,-0.382683432365086,0.923879532511289));
#18181=DIRECTION('ref_axis',(1.,0.,0.));
#18182=DIRECTION('',(-1.,0.,0.));
#18183=DIRECTION('center_axis',(0.,0.,1.));
#18184=DIRECTION('ref_axis',(1.,0.,0.));
#18185=DIRECTION('center_axis',(0.,0.,1.));
#18186=DIRECTION('ref_axis',(1.,0.,0.));
#18187=DIRECTION('',(0.754127675160995,-0.656727835222685,5.63512495882306E-15));
#18188=DIRECTION('center_axis',(0.,0.,1.));
#18189=DIRECTION('ref_axis',(1.,0.,0.));
#18190=DIRECTION('center_axis',(0.,0.,1.));
#18191=DIRECTION('ref_axis',(1.,0.,0.));
#18192=DIRECTION('',(0.,0.,-1.));
#18193=DIRECTION('center_axis',(0.,0.,-1.));
#18194=DIRECTION('ref_axis',(1.,0.,0.));
#18195=DIRECTION('center_axis',(0.,0.,-1.));
#18196=DIRECTION('ref_axis',(1.,0.,0.));
#18197=DIRECTION('center_axis',(0.,1.88765402986373E-15,-1.));
#18198=DIRECTION('ref_axis',(1.,3.04118571122536E-17,0.));
#18199=DIRECTION('center_axis',(0.,0.,-1.));
#18200=DIRECTION('ref_axis',(1.,6.12323399573677E-17,0.));
#18201=DIRECTION('',(-0.38268343236509,1.68546160473598E-15,-0.923879532511286));
#18202=DIRECTION('center_axis',(0.,0.,-1.));
#18203=DIRECTION('ref_axis',(1.,0.,0.));
#18204=DIRECTION('',(-0.707106781186548,-8.65956056235493E-17,-0.707106781186548));
#18205=DIRECTION('center_axis',(0.,0.,-1.));
#18206=DIRECTION('ref_axis',(-1.,0.,0.));
#18207=DIRECTION('center_axis',(-1.22464679914735E-16,-1.,0.));
#18208=DIRECTION('ref_axis',(1.,-1.22464679914735E-16,0.));
#18209=DIRECTION('center_axis',(0.,0.,1.));
#18210=DIRECTION('ref_axis',(1.,0.,0.));
#18211=DIRECTION('center_axis',(0.707106781186547,0.,-0.707106781186548));
#18212=DIRECTION('ref_axis',(-0.707106781186548,0.,-0.707106781186547));
#18213=DIRECTION('',(-0.577350269189627,0.577350269189624,-0.577350269189627));
#18214=DIRECTION('',(0.,1.,0.));
#18215=DIRECTION('',(0.707106781186548,0.,0.707106781186547));
#18216=DIRECTION('center_axis',(0.707106781186547,0.,-0.707106781186548));
#18217=DIRECTION('ref_axis',(-0.707106781186548,0.,-0.707106781186547));
#18218=DIRECTION('',(-0.577350269189627,0.577350269189624,-0.577350269189627));
#18219=DIRECTION('',(0.,1.,0.));
#18220=DIRECTION('',(0.577350269189627,0.577350269189624,0.577350269189627));
#18221=DIRECTION('center_axis',(0.,0.,1.));
#18222=DIRECTION('ref_axis',(-0.707106781186547,-0.707106781186547,0.));
#18223=DIRECTION('',(0.,-0.707106781186556,0.707106781186539));
#18224=DIRECTION('center_axis',(0.,0.,-1.));
#18225=DIRECTION('ref_axis',(-0.707106781186548,-0.707106781186548,0.));
#18226=DIRECTION('center_axis',(0.,0.,1.));
#18227=DIRECTION('ref_axis',(-0.707106781186548,-0.707106781186548,0.));
#18228=DIRECTION('center_axis',(0.,-0.707106781186547,-0.707106781186548));
#18229=DIRECTION('ref_axis',(-1.,0.,0.));
#18230=DIRECTION('',(0.,-0.707106781186548,0.707106781186547));
#18231=DIRECTION('',(-1.,0.,0.));
#18232=DIRECTION('',(1.,0.,0.));
#18233=DIRECTION('center_axis',(0.,0.,1.));
#18234=DIRECTION('ref_axis',(0.707106781186547,-0.707106781186547,0.));
#18235=DIRECTION('',(0.707106781186556,0.,0.707106781186539));
#18236=DIRECTION('center_axis',(0.,0.,-1.));
#18237=DIRECTION('ref_axis',(0.707106781186548,-0.707106781186548,0.));
#18238=DIRECTION('center_axis',(0.,0.,1.));
#18239=DIRECTION('ref_axis',(0.707106781186548,-0.707106781186548,0.));
#18240=DIRECTION('center_axis',(0.707106781186547,0.,-0.707106781186548));
#18241=DIRECTION('ref_axis',(-0.707106781186548,0.,-0.707106781186547));
#18242=DIRECTION('',(0.,1.,0.));
#18243=DIRECTION('',(0.577350269189627,0.577350269189624,0.577350269189627));
#18244=DIRECTION('center_axis',(0.,0.707106781186548,-0.707106781186548));
#18245=DIRECTION('ref_axis',(-1.,0.,0.));
#18246=DIRECTION('',(1.,0.,0.));
#18247=DIRECTION('',(0.,-0.707106781186548,-0.707106781186548));
#18248=DIRECTION('',(-1.,0.,0.));
#18249=DIRECTION('center_axis',(0.,0.,-1.));
#18250=DIRECTION('ref_axis',(0.,-1.,0.));
#18251=DIRECTION('',(0.,0.707106781186548,-0.707106781186548));
#18252=DIRECTION('center_axis',(0.,0.,-1.));
#18253=DIRECTION('ref_axis',(0.,-1.,0.));
#18254=DIRECTION('center_axis',(0.,0.,1.));
#18255=DIRECTION('ref_axis',(0.,-1.,0.));
#18256=DIRECTION('center_axis',(0.,-0.707106781186548,-0.707106781186548));
#18257=DIRECTION('ref_axis',(-1.,0.,0.));
#18258=DIRECTION('',(1.,0.,0.));
#18259=DIRECTION('',(-1.,0.,0.));
#18260=DIRECTION('center_axis',(0.,-0.707106781186548,-0.707106781186548));
#18261=DIRECTION('ref_axis',(-1.,0.,0.));
#18262=DIRECTION('',(-1.,0.,0.));
#18263=DIRECTION('',(0.,0.707106781186548,-0.707106781186548));
#18264=DIRECTION('',(1.,0.,0.));
#18265=DIRECTION('center_axis',(0.,0.,-1.));
#18266=DIRECTION('ref_axis',(0.,1.,0.));
#18267=DIRECTION('',(0.,-0.707106781186548,-0.707106781186548));
#18268=DIRECTION('center_axis',(0.,0.,-1.));
#18269=DIRECTION('ref_axis',(0.,1.,0.));
#18270=DIRECTION('center_axis',(0.,0.,1.));
#18271=DIRECTION('ref_axis',(0.,1.,0.));
#18272=DIRECTION('center_axis',(0.,0.707106781186548,-0.707106781186548));
#18273=DIRECTION('ref_axis',(-1.,0.,0.));
#18274=DIRECTION('',(-1.,0.,0.));
#18275=DIRECTION('',(1.,0.,0.));
#18276=DIRECTION('center_axis',(0.,0.707106781186548,-0.707106781186548));
#18277=DIRECTION('ref_axis',(-1.,0.,0.));
#18278=DIRECTION('',(1.,0.,0.));
#18279=DIRECTION('',(0.,-0.707106781186548,-0.707106781186548));
#18280=DIRECTION('',(-1.,0.,0.));
#18281=DIRECTION('center_axis',(0.,0.,-1.));
#18282=DIRECTION('ref_axis',(0.,-1.,0.));
#18283=DIRECTION('',(0.,0.707106781186548,-0.707106781186548));
#18284=DIRECTION('center_axis',(0.,0.,-1.));
#18285=DIRECTION('ref_axis',(0.,-1.,0.));
#18286=DIRECTION('center_axis',(0.,0.,1.));
#18287=DIRECTION('ref_axis',(0.,-1.,0.));
#18288=DIRECTION('center_axis',(0.,-0.707106781186548,-0.707106781186548));
#18289=DIRECTION('ref_axis',(-1.,0.,0.));
#18290=DIRECTION('',(1.,0.,0.));
#18291=DIRECTION('center_axis',(0.,-0.707106781186548,-0.707106781186548));
#18292=DIRECTION('ref_axis',(-1.,0.,0.));
#18293=DIRECTION('',(0.,0.707106781186548,-0.707106781186548));
#18294=DIRECTION('',(1.,0.,0.));
#18295=DIRECTION('center_axis',(0.,0.,-1.));
#18296=DIRECTION('ref_axis',(0.,1.,0.));
#18297=DIRECTION('',(0.,-0.707106781186548,-0.707106781186548));
#18298=DIRECTION('center_axis',(0.,0.,-1.));
#18299=DIRECTION('ref_axis',(0.,1.,0.));
#18300=DIRECTION('center_axis',(0.,0.,1.));
#18301=DIRECTION('ref_axis',(0.,1.,0.));
#18302=DIRECTION('center_axis',(0.,0.707106781186548,-0.707106781186548));
#18303=DIRECTION('ref_axis',(-1.,0.,0.));
#18304=DIRECTION('',(-1.,0.,0.));
#18305=DIRECTION('',(1.,0.,0.));
#18306=DIRECTION('center_axis',(0.,0.,1.));
#18307=DIRECTION('ref_axis',(0.707106781186547,0.707106781186547,0.));
#18308=DIRECTION('',(0.,0.707106781186556,0.707106781186539));
#18309=DIRECTION('center_axis',(0.,0.,1.));
#18310=DIRECTION('ref_axis',(0.707106781186548,0.707106781186548,0.));
#18311=DIRECTION('center_axis',(0.,0.707106781186547,-0.707106781186548));
#18312=DIRECTION('ref_axis',(-1.,0.,0.));
#18313=DIRECTION('',(0.,0.707106781186548,0.707106781186547));
#18314=DIRECTION('',(-1.,0.,0.));
#18315=DIRECTION('center_axis',(0.,0.,1.));
#18316=DIRECTION('ref_axis',(-0.707106781186547,0.707106781186547,0.));
#18317=DIRECTION('center_axis',(0.,0.,1.));
#18318=DIRECTION('ref_axis',(-0.707106781186548,0.707106781186548,0.));
#18319=DIRECTION('center_axis',(0.,0.,-1.));
#18320=DIRECTION('ref_axis',(0.,-1.,0.));
#18321=DIRECTION('',(0.,0.,-1.));
#18322=DIRECTION('center_axis',(0.,0.,-1.));
#18323=DIRECTION('ref_axis',(0.,-1.,0.));
#18324=DIRECTION('center_axis',(0.,-1.,0.));
#18325=DIRECTION('ref_axis',(-1.,0.,0.));
#18326=DIRECTION('',(-1.,0.,0.));
#18327=DIRECTION('center_axis',(0.,1.,0.));
#18328=DIRECTION('ref_axis',(1.,0.,0.));
#18329=DIRECTION('',(0.,0.,-1.));
#18330=DIRECTION('',(1.,0.,0.));
#18331=DIRECTION('center_axis',(0.,0.,-1.));
#18332=DIRECTION('ref_axis',(0.,-1.,0.));
#18333=DIRECTION('',(0.,0.,-1.));
#18334=DIRECTION('center_axis',(0.,0.,-1.));
#18335=DIRECTION('ref_axis',(0.,-1.,0.));
#18336=DIRECTION('center_axis',(0.,-1.,0.));
#18337=DIRECTION('ref_axis',(-1.,0.,0.));
#18338=DIRECTION('',(-1.,0.,0.));
#18339=DIRECTION('center_axis',(0.,0.,1.));
#18340=DIRECTION('ref_axis',(1.,0.,0.));
#18341=DIRECTION('center_axis',(0.,0.,-1.));
#18342=DIRECTION('ref_axis',(-0.707106781186547,-0.707106781186547,0.));
#18343=DIRECTION('center_axis',(0.,0.,1.));
#18344=DIRECTION('ref_axis',(-0.707106781186548,-0.707106781186548,0.));
#18345=DIRECTION('',(0.,0.70710678118655,0.707106781186545));
#18346=DIRECTION('center_axis',(0.,-0.707106781186548,0.707106781186548));
#18347=DIRECTION('ref_axis',(1.,0.,0.));
#18348=DIRECTION('',(1.,0.,0.));
#18349=DIRECTION('',(0.,0.707106781186548,0.707106781186548));
#18350=DIRECTION('center_axis',(0.,0.,-1.));
#18351=DIRECTION('ref_axis',(0.707106781186547,-0.707106781186547,0.));
#18352=DIRECTION('center_axis',(0.,0.,1.));
#18353=DIRECTION('ref_axis',(0.707106781186548,-0.707106781186548,0.));
#18354=DIRECTION('center_axis',(0.,-0.707106781186548,0.707106781186548));
#18355=DIRECTION('ref_axis',(1.,0.,0.));
#18356=DIRECTION('',(0.,0.707106781186548,0.707106781186548));
#18357=DIRECTION('center_axis',(0.,0.,1.));
#18358=DIRECTION('ref_axis',(0.,-1.,0.));
#18359=DIRECTION('',(0.,-0.707106781186548,0.707106781186548));
#18360=DIRECTION('center_axis',(0.,0.707106781186548,0.707106781186548));
#18361=DIRECTION('ref_axis',(1.,0.,0.));
#18362=DIRECTION('center_axis',(0.,0.,1.));
#18363=DIRECTION('ref_axis',(0.,1.,0.));
#18364=DIRECTION('center_axis',(0.,0.,-1.));
#18365=DIRECTION('ref_axis',(0.,1.,0.));
#18366=DIRECTION('center_axis',(0.,0.,1.));
#18367=DIRECTION('ref_axis',(0.,-1.,0.));
#18368=DIRECTION('',(0.,-0.707106781186548,0.707106781186548));
#18369=DIRECTION('center_axis',(0.,0.707106781186548,0.707106781186548));
#18370=DIRECTION('ref_axis',(1.,0.,0.));
#18371=DIRECTION('center_axis',(0.,0.,1.));
#18372=DIRECTION('ref_axis',(0.,1.,0.));
#18373=DIRECTION('center_axis',(0.,0.,-1.));
#18374=DIRECTION('ref_axis',(0.,1.,0.));
#18375=DIRECTION('center_axis',(0.,0.,1.));
#18376=DIRECTION('ref_axis',(0.707106781186547,-0.707106781186547,0.));
#18377=DIRECTION('',(0.,0.,-1.));
#18378=DIRECTION('center_axis',(0.,-1.,0.));
#18379=DIRECTION('ref_axis',(1.,0.,0.));
#18380=DIRECTION('',(0.,0.,1.));
#18381=DIRECTION('center_axis',(0.,0.,1.));
#18382=DIRECTION('ref_axis',(-0.707106781186547,-0.707106781186547,0.));
#18383=DIRECTION('center_axis',(0.,-1.,0.));
#18384=DIRECTION('ref_axis',(-1.,0.,0.));
#18385=DIRECTION('',(0.,0.,-1.));
#18386=DIRECTION('center_axis',(0.,0.,-1.));
#18387=DIRECTION('ref_axis',(0.,1.,0.));
#18388=DIRECTION('center_axis',(0.,-1.,0.));
#18389=DIRECTION('ref_axis',(-1.,0.,0.));
#18390=DIRECTION('',(0.,0.,-1.));
#18391=DIRECTION('center_axis',(0.,1.,0.));
#18392=DIRECTION('ref_axis',(1.,0.,0.));
#18393=DIRECTION('',(0.,0.,-1.));
#18394=DIRECTION('center_axis',(0.,0.,-1.));
#18395=DIRECTION('ref_axis',(0.,1.,0.));
#21834=CARTESIAN_POINT('',(0.,0.,0.));
#21835=CARTESIAN_POINT('Origin',(3.985,-1.16,0.4));
#21836=CARTESIAN_POINT('',(3.985,-1.16,0.0250000000000002));
#21837=CARTESIAN_POINT('',(4.,-1.145,0.04));
#21838=CARTESIAN_POINT('',(3.98916666666667,-1.15583333333333,0.0291666666666659));
#21839=CARTESIAN_POINT('',(4.,-1.145,0.74));
#21840=CARTESIAN_POINT('',(4.,-1.145,0.4));
#21841=CARTESIAN_POINT('',(3.985,-1.16,0.755));
#21842=CARTESIAN_POINT('',(3.9825,-1.1625,0.757500000000001));
#21843=CARTESIAN_POINT('',(3.97,-1.175,0.74));
#21844=CARTESIAN_POINT('',(3.44166666666668,-1.70333333333333,0.211666666666669));
#21845=CARTESIAN_POINT('',(3.97,-1.175,0.04));
#21846=CARTESIAN_POINT('',(3.97,-1.175,0.4));
#21847=CARTESIAN_POINT('',(3.43500000000001,-1.71,0.574999999999998));
#21848=CARTESIAN_POINT('Origin',(1.05,-1.145,0.77));
#21849=CARTESIAN_POINT('',(3.9612132034356,-1.1362132034356,0.778786796564403));
#21850=CARTESIAN_POINT('',(3.94,-1.115,0.8));
#21851=CARTESIAN_POINT('',(2.1,-1.1362132034356,0.778786796564404));
#21852=CARTESIAN_POINT('',(0.525,-1.1362132034356,0.778786796564404));
#21853=CARTESIAN_POINT('',(2.1,-1.175,0.74));
#21854=CARTESIAN_POINT('',(2.1,-1.175,0.74));
#21855=CARTESIAN_POINT('',(1.05,-1.175,0.74));
#21856=CARTESIAN_POINT('Origin',(3.97,-1.5,0.77));
#21857=CARTESIAN_POINT('',(4.,1.145,0.74));
#21858=CARTESIAN_POINT('',(4.,-1.5,0.74));
#21859=CARTESIAN_POINT('',(3.985,1.16,0.755));
#21860=CARTESIAN_POINT('',(4.4825,0.662499999999977,0.257499999999996));
#21861=CARTESIAN_POINT('',(3.9612132034356,1.1362132034356,0.778786796564404));
#21862=CARTESIAN_POINT('',(3.94,1.115,0.8));
#21863=CARTESIAN_POINT('',(3.9612132034356,-0.75,0.778786796564403));
#21864=CARTESIAN_POINT('Origin',(4.,-3.,0.));
#21865=CARTESIAN_POINT('',(4.,1.145,0.04));
#21866=CARTESIAN_POINT('',(4.,-1.5,0.04));
#21867=CARTESIAN_POINT('',(4.,1.145,0.4));
#21868=CARTESIAN_POINT('Origin',(3.985,1.16,0.4));
#21869=CARTESIAN_POINT('',(3.985,1.16,0.0250000000000001));
#21870=CARTESIAN_POINT('',(4.48916666666667,0.65583333333331,0.52916666666667));
#21871=CARTESIAN_POINT('',(3.97,1.175,0.04));
#21872=CARTESIAN_POINT('',(3.60166666666668,1.54333333333333,0.408333333333331));
#21873=CARTESIAN_POINT('',(3.97,1.175,0.74));
#21874=CARTESIAN_POINT('',(3.97,1.175,0.4));
#21875=CARTESIAN_POINT('',(3.60833333333335,1.53666666666666,0.378333333333336));
#21876=CARTESIAN_POINT('Origin',(2.05,1.145,0.77));
#21877=CARTESIAN_POINT('',(2.1,1.175,0.74));
#21878=CARTESIAN_POINT('',(2.05,1.175,0.74));
#21879=CARTESIAN_POINT('',(2.1,1.1362132034356,0.778786796564404));
#21880=CARTESIAN_POINT('',(2.1,1.175,0.74));
#21881=CARTESIAN_POINT('',(1.025,1.1362132034356,0.778786796564404));
#21882=CARTESIAN_POINT('Origin',(3.985,-1.84,0.4));
#21883=CARTESIAN_POINT('',(3.985,-1.84,0.755));
#21884=CARTESIAN_POINT('',(4.,-1.855,0.74));
#21885=CARTESIAN_POINT('',(3.9825,-1.8375,0.757500000000001));
#21886=CARTESIAN_POINT('',(4.,-1.855,0.04));
#21887=CARTESIAN_POINT('',(4.,-1.855,0.4));
#21888=CARTESIAN_POINT('',(3.985,-1.84,0.0250000000000002));
#21889=CARTESIAN_POINT('',(3.98916666666666,-1.84416666666666,0.029166666666665));
#21890=CARTESIAN_POINT('',(3.97,-1.825,0.04));
#21891=CARTESIAN_POINT('',(3.60166666666668,-1.45666666666667,0.408333333333331));
#21892=CARTESIAN_POINT('',(3.97,-1.825,0.74));
#21893=CARTESIAN_POINT('',(3.97,-1.825,0.4));
#21894=CARTESIAN_POINT('',(3.60833333333335,-1.46333333333334,0.378333333333335));
#21895=CARTESIAN_POINT('Origin',(4.,-3.,0.));
#21896=CARTESIAN_POINT('',(4.,-2.6,0.74));
#21897=CARTESIAN_POINT('',(4.,-1.5,0.74));
#21898=CARTESIAN_POINT('',(4.,-2.6,0.04));
#21899=CARTESIAN_POINT('',(4.,-2.6,0.));
#21900=CARTESIAN_POINT('',(4.,-1.5,0.04));
#21901=CARTESIAN_POINT('Origin',(3.97,-1.5,0.77));
#21902=CARTESIAN_POINT('',(3.9612132034356,-1.8637867965644,0.778786796564404));
#21903=CARTESIAN_POINT('',(3.94,-1.885,0.8));
#21904=CARTESIAN_POINT('',(3.9612132034356,-2.6,0.778786796564403));
#21905=CARTESIAN_POINT('',(3.9612132034356,-0.75,0.778786796564403));
#21906=CARTESIAN_POINT('',(4.,-2.6,0.74));
#21907=CARTESIAN_POINT('Origin',(2.05,-1.855,0.77));
#21908=CARTESIAN_POINT('',(2.1,-1.825,0.74));
#21909=CARTESIAN_POINT('',(2.05,-1.825,0.74));
#21910=CARTESIAN_POINT('',(2.1,-1.8637867965644,0.778786796564404));
#21911=CARTESIAN_POINT('',(2.1,-1.825,0.74));
#21912=CARTESIAN_POINT('',(1.025,-1.8637867965644,0.778786796564404));
#21913=CARTESIAN_POINT('Origin',(-3.985,-1.84,0.4));
#21914=CARTESIAN_POINT('',(-3.985,-1.84,0.0250000000000001));
#21915=CARTESIAN_POINT('',(-4.,-1.855,0.04));
#21916=CARTESIAN_POINT('',(-3.48916666666666,-1.34416666666665,-0.470833333333338));
#21917=CARTESIAN_POINT('',(-4.,-1.855,0.74));
#21918=CARTESIAN_POINT('',(-4.,-1.855,0.4));
#21919=CARTESIAN_POINT('',(-3.985,-1.84,0.755));
#21920=CARTESIAN_POINT('',(-3.4825,-1.33749999999998,1.2575));
#21921=CARTESIAN_POINT('',(-3.97,-1.825,0.74));
#21922=CARTESIAN_POINT('',(-3.44166666666668,-1.29666666666667,0.21166666666667));
#21923=CARTESIAN_POINT('',(-3.97,-1.825,0.04));
#21924=CARTESIAN_POINT('',(-3.97,-1.825,0.4));
#21925=CARTESIAN_POINT('',(-3.43500000000002,-1.29,0.574999999999997));
#21926=CARTESIAN_POINT('Origin',(-3.97,1.5,0.77));
#21927=CARTESIAN_POINT('',(-4.,-2.6,0.74));
#21928=CARTESIAN_POINT('',(-4.,1.5,0.74));
#21929=CARTESIAN_POINT('',(-3.9612132034356,-2.6,0.778786796564404));
#21930=CARTESIAN_POINT('',(-4.,-2.6,0.74));
#21931=CARTESIAN_POINT('',(-3.9612132034356,-1.8637867965644,0.778786796564403));
#21932=CARTESIAN_POINT('',(-3.9612132034356,0.75,0.778786796564403));
#21933=CARTESIAN_POINT('',(-3.94,-1.885,0.8));
#21934=CARTESIAN_POINT('Origin',(-4.,3.,0.));
#21935=CARTESIAN_POINT('',(-4.,-2.6,0.04));
#21936=CARTESIAN_POINT('',(-4.,1.5,0.04));
#21937=CARTESIAN_POINT('',(-4.,-2.6,0.));
#21938=CARTESIAN_POINT('Origin',(-3.98,1.5,0.02));
#21939=CARTESIAN_POINT('',(-3.96,-1.865,0.));
#21940=CARTESIAN_POINT('',(-4.,-1.825,0.04));
#21941=CARTESIAN_POINT('',(-3.96,-2.6,0.));
#21942=CARTESIAN_POINT('',(-3.96,1.5,0.));
#21943=CARTESIAN_POINT('',(-3.96,-2.6,0.));
#21944=CARTESIAN_POINT('Origin',(-3.985,-1.16,0.4));
#21945=CARTESIAN_POINT('',(-3.985,-1.16,0.755));
#21946=CARTESIAN_POINT('',(-4.,-1.145,0.74));
#21947=CARTESIAN_POINT('',(-4.4825,-0.662499999999977,0.257499999999996));
#21948=CARTESIAN_POINT('',(-4.,-1.145,0.04));
#21949=CARTESIAN_POINT('',(-4.,-1.145,0.4));
#21950=CARTESIAN_POINT('',(-3.985,-1.16,0.0250000000000001));
#21951=CARTESIAN_POINT('',(-4.48916666666667,-0.65583333333331,0.52916666666667));
#21952=CARTESIAN_POINT('',(-3.97,-1.175,0.04));
#21953=CARTESIAN_POINT('',(-3.60166666666668,-1.54333333333333,0.408333333333331));
#21954=CARTESIAN_POINT('',(-3.97,-1.175,0.74));
#21955=CARTESIAN_POINT('',(-3.97,-1.175,0.4));
#21956=CARTESIAN_POINT('',(-3.60833333333335,-1.53666666666666,0.378333333333336));
#21957=CARTESIAN_POINT('Origin',(-3.98,1.5,0.02));
#21958=CARTESIAN_POINT('',(-4.,1.145,0.04));
#21959=CARTESIAN_POINT('',(-4.,1.5,0.04));
#21960=CARTESIAN_POINT('',(-3.985,1.16,0.0250000000000002));
#21961=CARTESIAN_POINT('',(-3.98916666666667,1.15583333333333,0.0291666666666659));
#21962=CARTESIAN_POINT('',(-3.96,1.135,0.));
#21963=CARTESIAN_POINT('',(-4.,1.175,0.04));
#21964=CARTESIAN_POINT('',(-3.96,-1.135,0.));
#21965=CARTESIAN_POINT('',(-3.96,1.5,0.));
#21966=CARTESIAN_POINT('',(-3.96,-1.135,0.));
#21967=CARTESIAN_POINT('Origin',(-4.,3.,0.));
#21968=CARTESIAN_POINT('',(-4.,1.145,0.74));
#21969=CARTESIAN_POINT('',(-4.,1.5,0.74));
#21970=CARTESIAN_POINT('',(-4.,1.145,0.4));
#21971=CARTESIAN_POINT('Origin',(-3.97,1.5,0.77));
#21972=CARTESIAN_POINT('',(-3.9612132034356,-1.1362132034356,0.778786796564404));
#21973=CARTESIAN_POINT('',(-3.94,-1.115,0.8));
#21974=CARTESIAN_POINT('',(-3.9612132034356,1.1362132034356,0.778786796564403));
#21975=CARTESIAN_POINT('',(-3.9612132034356,0.75,0.778786796564403));
#21976=CARTESIAN_POINT('',(-3.985,1.16,0.755));
#21977=CARTESIAN_POINT('',(-3.94,1.115,0.8));
#21978=CARTESIAN_POINT('',(-3.9825,1.1625,0.757500000000001));
#21979=CARTESIAN_POINT('Origin',(-3.985,1.16,0.4));
#21980=CARTESIAN_POINT('',(-3.97,1.175,0.74));
#21981=CARTESIAN_POINT('',(-3.44166666666668,1.70333333333333,0.211666666666669));
#21982=CARTESIAN_POINT('',(-3.97,1.175,0.04));
#21983=CARTESIAN_POINT('',(-3.97,1.175,0.4));
#21984=CARTESIAN_POINT('',(-3.43500000000001,1.71,0.574999999999998));
#21985=CARTESIAN_POINT('Origin',(0.,-3.14975114354414E-17,1.9893933982822));
#21986=CARTESIAN_POINT('',(-1.0287867965644,2.46519032881566E-32,1.9787867965644));
#21987=CARTESIAN_POINT('Origin',(0.,-6.29950228708828E-17,1.9787867965644));
#21988=CARTESIAN_POINT('',(-1.08,-1.32261854307914E-16,2.));
#21989=CARTESIAN_POINT('',(-1.0543933982822,6.61309271539571E-17,1.9893933982822));
#21990=CARTESIAN_POINT('Origin',(0.,0.,2.));
#21991=CARTESIAN_POINT('Origin',(0.,0.,1.975));
#21992=CARTESIAN_POINT('',(-1.0212132034356,-2.50125096166884E-16,1.9712132034356));
#21993=CARTESIAN_POINT('',(-1.025,-1.25526296912604E-16,1.975));
#21994=CARTESIAN_POINT('Origin',(0.,-6.25312740417209E-17,1.9712132034356));
#21995=CARTESIAN_POINT('Origin',(0.,0.,2.));
#21996=CARTESIAN_POINT('',(-1.54,1.88595607068692E-16,2.));
#21997=CARTESIAN_POINT('Origin',(0.,0.,2.));
#21998=CARTESIAN_POINT('Origin',(0.,-3.12656370208604E-17,1.9456066017178));
#21999=CARTESIAN_POINT('',(-1.,1.22464679914735E-16,1.92));
#22000=CARTESIAN_POINT('',(-1.0106066017178,-1.86294888040809E-16,1.9456066017178));
#22001=CARTESIAN_POINT('Origin',(0.,0.,1.92));
#22002=CARTESIAN_POINT('Origin',(0.,0.,2.));
#22003=CARTESIAN_POINT('',(-1.,-1.22464679914735E-16,0.4));
#22004=CARTESIAN_POINT('',(-1.,1.22464679914735E-16,2.));
#22005=CARTESIAN_POINT('Origin',(0.,0.,0.4));
#22006=CARTESIAN_POINT('',(0.234267305685713,0.972172222132867,1.4));
#22007=CARTESIAN_POINT('Ctrl Pts',(0.234267305685713,0.972172222132867,
1.4));
#22008=CARTESIAN_POINT('Ctrl Pts',(0.234267305685713,0.972172222132867,
1.43391900663149));
#22009=CARTESIAN_POINT('Ctrl Pts',(0.217453199576997,0.97640750358249,1.50750370302361));
#22010=CARTESIAN_POINT('Ctrl Pts',(0.162557143889187,0.987394406811514,
1.57537359399088));
#22011=CARTESIAN_POINT('Ctrl Pts',(0.103338063857534,0.99504750544363,1.61334001682052));
#22012=CARTESIAN_POINT('Ctrl Pts',(0.0342814671797575,1.00049861473999,
1.63725191259632));
#22013=CARTESIAN_POINT('Ctrl Pts',(-0.0343654764701675,1.00042505413025,
1.63680882232891));
#22014=CARTESIAN_POINT('Ctrl Pts',(-0.103211592970685,0.995066437220061,
1.61345114045812));
#22015=CARTESIAN_POINT('Ctrl Pts',(-0.148329808958505,0.989169324847084,
1.58415597304455));
#22016=CARTESIAN_POINT('Ctrl Pts',(-0.183849662047555,0.983122988023421,
1.54896583267799));
#22017=CARTESIAN_POINT('Ctrl Pts',(-0.222528948857546,0.975130828482948,
1.48743715896112));
#22018=CARTESIAN_POINT('Ctrl Pts',(-0.242031304986677,0.970123636918925,
1.40006630054004));
#22019=CARTESIAN_POINT('Ctrl Pts',(-0.222407063698446,0.975220619502292,
1.31224680544824));
#22020=CARTESIAN_POINT('Ctrl Pts',(-0.183657702453494,0.983122398337006,
1.25122736917816));
#22021=CARTESIAN_POINT('Ctrl Pts',(-0.13684634930182,0.991308187330295,
1.20344105854914));
#22022=CARTESIAN_POINT('Ctrl Pts',(-0.0520840197900239,1.0005765283454,
1.16234073969225));
#22023=CARTESIAN_POINT('Ctrl Pts',(0.0343068301640742,1.00047914632208,
1.16292703932357));
#22024=CARTESIAN_POINT('Ctrl Pts',(0.10329410020646,0.995062702176677,1.18658091767974));
#22025=CARTESIAN_POINT('Ctrl Pts',(0.162577481379246,0.987395818375031,
1.22465007697402));
#22026=CARTESIAN_POINT('Ctrl Pts',(0.217435775063741,0.97641259628012,1.29246754064607));
#22027=CARTESIAN_POINT('Ctrl Pts',(0.234267305685713,0.972172222132867,
1.36608099336852));
#22028=CARTESIAN_POINT('Ctrl Pts',(0.234267305685713,0.972172222132867,
1.4));
#22029=CARTESIAN_POINT('Ctrl Pts',(0.234267305685713,0.972172222132867,
1.4));
#22030=CARTESIAN_POINT('Ctrl Pts',(0.234267305685713,0.972172222132867,
1.36608099336852));
#22031=CARTESIAN_POINT('Ctrl Pts',(0.217435775063741,0.97641259628012,1.29246754064607));
#22032=CARTESIAN_POINT('Ctrl Pts',(0.162577481379246,0.987395818375031,
1.22465007697402));
#22033=CARTESIAN_POINT('Ctrl Pts',(0.10329410020646,0.995062702176677,1.18658091767974));
#22034=CARTESIAN_POINT('Ctrl Pts',(0.0343068301640742,1.00047914632208,
1.16292703932357));
#22035=CARTESIAN_POINT('Ctrl Pts',(-0.0520840197900239,1.0005765283454,
1.16234073969225));
#22036=CARTESIAN_POINT('Ctrl Pts',(-0.13684634930182,0.991308187330295,
1.20344105854914));
#22037=CARTESIAN_POINT('Ctrl Pts',(-0.183657702453494,0.983122398337006,
1.25122736917816));
#22038=CARTESIAN_POINT('Ctrl Pts',(-0.222407063698446,0.975220619502292,
1.31224680544824));
#22039=CARTESIAN_POINT('Ctrl Pts',(-0.242031304986677,0.970123636918925,
1.40006630054004));
#22040=CARTESIAN_POINT('Ctrl Pts',(-0.222528948857546,0.975130828482948,
1.48743715896112));
#22041=CARTESIAN_POINT('Ctrl Pts',(-0.183849662047555,0.983122988023421,
1.54896583267799));
#22042=CARTESIAN_POINT('Ctrl Pts',(-0.148329808958505,0.989169324847084,
1.58415597304455));
#22043=CARTESIAN_POINT('Ctrl Pts',(-0.103211592970685,0.995066437220061,
1.61345114045812));
#22044=CARTESIAN_POINT('Ctrl Pts',(-0.0343654764701675,1.00042505413025,
1.63680882232891));
#22045=CARTESIAN_POINT('Ctrl Pts',(0.0342814671797575,1.00049861473999,
1.63725191259632));
#22046=CARTESIAN_POINT('Ctrl Pts',(0.103338063857534,0.99504750544363,1.61334001682052));
#22047=CARTESIAN_POINT('Ctrl Pts',(0.162557143889187,0.987394406811514,
1.57537359399088));
#22048=CARTESIAN_POINT('Ctrl Pts',(0.217453199576997,0.97640750358249,1.50750370302361));
#22049=CARTESIAN_POINT('Ctrl Pts',(0.234267305685713,0.972172222132867,
1.43391900663149));
#22050=CARTESIAN_POINT('Ctrl Pts',(0.234267305685713,0.972172222132867,
1.4));
#22051=CARTESIAN_POINT('Ctrl Pts',(0.224511537123809,0.984368805790859,
1.4));
#22052=CARTESIAN_POINT('Ctrl Pts',(0.224511537123809,0.984368805790859,
1.36785293603036));
#22053=CARTESIAN_POINT('Ctrl Pts',(0.208715983620224,0.988232116107654,
1.29804318701526));
#22054=CARTESIAN_POINT('Ctrl Pts',(0.156597374287794,0.998329294088653,
1.23289572937968));
#22055=CARTESIAN_POINT('Ctrl Pts',(0.0996850231726542,1.00542138378364,
1.19601708761738));
#22056=CARTESIAN_POINT('Ctrl Pts',(0.0331933469447592,1.01044296116397,
1.17298582817999));
#22057=CARTESIAN_POINT('Ctrl Pts',(-0.0504018911245414,1.01053249517299,
1.17242112850164));
#22058=CARTESIAN_POINT('Ctrl Pts',(-0.131966316236839,1.00194232959414,
1.21241761585945));
#22059=CARTESIAN_POINT('Ctrl Pts',(-0.176623835810546,0.994399145207215,
1.25842866128864));
#22060=CARTESIAN_POINT('Ctrl Pts',(-0.21338883997175,0.987146498650659,
1.31681134873593));
#22061=CARTESIAN_POINT('Ctrl Pts',(-0.231784665389821,0.982502518259946,
1.40006723250035));
#22062=CARTESIAN_POINT('Ctrl Pts',(-0.213493242367903,0.987065442519242,
1.48288286604478));
#22063=CARTESIAN_POINT('Ctrl Pts',(-0.176810077065311,0.994399827877688,
1.54175634937481));
#22064=CARTESIAN_POINT('Ctrl Pts',(-0.142905163319919,0.999972627766867,
1.5756422556539));
#22065=CARTESIAN_POINT('Ctrl Pts',(-0.099608650549313,1.00542488505706,
1.60401383731078));
#22066=CARTESIAN_POINT('Ctrl Pts',(-0.03323883765608,1.01039449521007,1.62676344662667));
#22067=CARTESIAN_POINT('Ctrl Pts',(0.033164982119191,1.01046069537358,1.62718522868402));
#22068=CARTESIAN_POINT('Ctrl Pts',(0.0997312542373632,1.00540762238061,
1.60390736404938));
#22069=CARTESIAN_POINT('Ctrl Pts',(0.156576887349813,0.998328050935301,
1.56712687096736));
#22070=CARTESIAN_POINT('Ctrl Pts',(0.208734202187127,0.988227502023521,
1.50192933822754));
#22071=CARTESIAN_POINT('Ctrl Pts',(0.224511537123809,0.984368805790859,
1.43214706396964));
#22072=CARTESIAN_POINT('Ctrl Pts',(0.224511537123809,0.984368805790859,
1.4));
#22073=CARTESIAN_POINT('Ctrl Pts',(0.214755768561905,0.996565389448851,
1.4));
#22074=CARTESIAN_POINT('Ctrl Pts',(0.214755768561905,0.996565389448851,
1.36962487869221));
#22075=CARTESIAN_POINT('Ctrl Pts',(0.199996192176708,1.00005163593519,1.30361883338444));
#22076=CARTESIAN_POINT('Ctrl Pts',(0.150617267196342,1.00926276980227,1.24114138178534));
#22077=CARTESIAN_POINT('Ctrl Pts',(0.096075946138849,1.01578006539061,1.20545325755502));
#22078=CARTESIAN_POINT('Ctrl Pts',(0.0320798637254439,1.02040677600585,
1.18304461703641));
#22079=CARTESIAN_POINT('Ctrl Pts',(-0.0487197624590589,1.02048846200059,
1.18250151731103));
#22080=CARTESIAN_POINT('Ctrl Pts',(-0.127086283171857,1.01257647185799,
1.22139417316976));
#22081=CARTESIAN_POINT('Ctrl Pts',(-0.169589969167599,1.00567589207742,
1.26562995339912));
#22082=CARTESIAN_POINT('Ctrl Pts',(-0.204370616245054,0.999072377799025,
1.32137589202362));
#22083=CARTESIAN_POINT('Ctrl Pts',(-0.221538025792965,0.994881399600966,
1.40006816446067));
#22084=CARTESIAN_POINT('Ctrl Pts',(-0.20445753587826,0.999000056555535,
1.47832857312844));
#22085=CARTESIAN_POINT('Ctrl Pts',(-0.169770492083067,1.00567666773195,
1.53454686607163));
#22086=CARTESIAN_POINT('Ctrl Pts',(-0.137480517681333,1.01077593068665,
1.56712853826326));
#22087=CARTESIAN_POINT('Ctrl Pts',(-0.0960057081279411,1.01578333289406,
1.59457653416343));
#22088=CARTESIAN_POINT('Ctrl Pts',(-0.0321121988419924,1.02036393628989,
1.61671807092442));
#22089=CARTESIAN_POINT('Ctrl Pts',(0.0320484970586246,1.02042277600718,
1.61711854477173));
#22090=CARTESIAN_POINT('Ctrl Pts',(0.0961244446171922,1.01576773931759,
1.59447471127824));
#22091=CARTESIAN_POINT('Ctrl Pts',(0.150596630810439,1.00926169505909,1.55888014794385));
#22092=CARTESIAN_POINT('Ctrl Pts',(0.200015204797257,1.00004750046455,1.49635497343148));
#22093=CARTESIAN_POINT('Ctrl Pts',(0.214755768561905,0.996565389448851,
1.43037512130779));
#22094=CARTESIAN_POINT('Ctrl Pts',(0.214755768561905,0.996565389448851,
1.4));
#22095=CARTESIAN_POINT('Ctrl Pts',(0.205,1.00876197310684,1.4));
#22096=CARTESIAN_POINT('Ctrl Pts',(0.205,1.00876197310684,1.37139682135405));
#22097=CARTESIAN_POINT('Ctrl Pts',(0.191276400733191,1.01187115576272,1.30919447975363));
#22098=CARTESIAN_POINT('Ctrl Pts',(0.14463716010489,1.0201962455159,1.249387034191));
#22099=CARTESIAN_POINT('Ctrl Pts',(0.0924668691050436,1.02613874699757,
1.21488942749266));
#22100=CARTESIAN_POINT('Ctrl Pts',(0.0309663805061289,1.03037059084774,
1.19310340589283));
#22101=CARTESIAN_POINT('Ctrl Pts',(-0.0470376337935765,1.03044442882818,
1.19258190612042));
#22102=CARTESIAN_POINT('Ctrl Pts',(-0.122206250106876,1.02321061412184,
1.23037073048007));
#22103=CARTESIAN_POINT('Ctrl Pts',(-0.162556102524651,1.01695263894763,
1.2728312455096));
#22104=CARTESIAN_POINT('Ctrl Pts',(-0.195352392518359,1.01099825694739,
1.3259404353113));
#22105=CARTESIAN_POINT('Ctrl Pts',(-0.211291386196109,1.00726028094199,
1.40006909642098));
#22106=CARTESIAN_POINT('Ctrl Pts',(-0.195421829388617,1.01093467059183,
1.47377428021209));
#22107=CARTESIAN_POINT('Ctrl Pts',(-0.162730907100823,1.01695350758622,
1.52733738276844));
#22108=CARTESIAN_POINT('Ctrl Pts',(-0.132055872042747,1.02157923360643,
1.55861482087262));
#22109=CARTESIAN_POINT('Ctrl Pts',(-0.0924027657065692,1.02614178073107,
1.58513923101609));
#22110=CARTESIAN_POINT('Ctrl Pts',(-0.0309855600279049,1.03033337736971,
1.60667269522218));
#22111=CARTESIAN_POINT('Ctrl Pts',(0.0309320119980581,1.03038485664077,
1.60705186085944));
#22112=CARTESIAN_POINT('Ctrl Pts',(0.0925176349970211,1.02612785625456,
1.58504205850711));
#22113=CARTESIAN_POINT('Ctrl Pts',(0.144616374271065,1.02019533918288,1.55063342492034));
#22114=CARTESIAN_POINT('Ctrl Pts',(0.191296207407388,1.01186749890558,1.49078060863542));
#22115=CARTESIAN_POINT('Ctrl Pts',(0.205,1.00876197310684,1.42860317864595));
#22116=CARTESIAN_POINT('Ctrl Pts',(0.205,1.00876197310684,1.4));
#22117=CARTESIAN_POINT('',(0.205,1.00876197310684,1.4));
#22118=CARTESIAN_POINT('',(0.234267305685713,0.972172222132867,1.4));
#22119=CARTESIAN_POINT('',(-0.000185900815659297,1.03004010593546,1.19476336551356));
#22120=CARTESIAN_POINT('Ctrl Pts',(0.205,1.00876197310684,1.4));
#22121=CARTESIAN_POINT('Ctrl Pts',(0.205,1.00876197310684,1.37139682135405));
#22122=CARTESIAN_POINT('Ctrl Pts',(0.191276400733191,1.01187115576272,1.30919447975363));
#22123=CARTESIAN_POINT('Ctrl Pts',(0.14463716010489,1.0201962455159,1.249387034191));
#22124=CARTESIAN_POINT('Ctrl Pts',(0.0924668691050436,1.02613874699757,
1.21488942749266));
#22125=CARTESIAN_POINT('Ctrl Pts',(0.0463415026558576,1.0293126298852,1.19854991129279));
#22126=CARTESIAN_POINT('Ctrl Pts',(0.0152903507427837,1.03003762732168,
1.19477984108684));
#22127=CARTESIAN_POINT('Ctrl Pts',(-0.000201953715795163,1.03004356916167,
1.19474293166142));
#22128=CARTESIAN_POINT('Ctrl Pts',(-0.000201953715795163,1.03004356916167,
1.19474293166142));
#22129=CARTESIAN_POINT('Ctrl Pts',(-0.015694258174374,1.03004951100166,
1.19470602223599));
#22130=CARTESIAN_POINT('Ctrl Pts',(-0.0620713570562364,1.02899766588691,
1.20013967099235));
#22131=CARTESIAN_POINT('Ctrl Pts',(-0.122206250106876,1.02321061412184,
1.23037073048007));
#22132=CARTESIAN_POINT('Ctrl Pts',(-0.162556102524651,1.01695263894763,
1.2728312455096));
#22133=CARTESIAN_POINT('Ctrl Pts',(-0.195352392518359,1.01099825694739,
1.3259404353113));
#22134=CARTESIAN_POINT('Ctrl Pts',(-0.211291386196109,1.00726028094199,
1.40006909642098));
#22135=CARTESIAN_POINT('Ctrl Pts',(-0.195421829388617,1.01093467059183,
1.47377428021209));
#22136=CARTESIAN_POINT('Ctrl Pts',(-0.162730907100823,1.01695350758622,
1.52733738276844));
#22137=CARTESIAN_POINT('Ctrl Pts',(-0.132055872042747,1.02157923360643,
1.55861482087262));
#22138=CARTESIAN_POINT('Ctrl Pts',(-0.0924027657065692,1.02614178073107,
1.58513923101609));
#22139=CARTESIAN_POINT('Ctrl Pts',(-0.0309855600279049,1.03033337736971,
1.60667269522218));
#22140=CARTESIAN_POINT('Ctrl Pts',(0.0309320119980581,1.03038485664077,
1.60705186085944));
#22141=CARTESIAN_POINT('Ctrl Pts',(0.0925176349970211,1.02612785625456,
1.58504205850711));
#22142=CARTESIAN_POINT('Ctrl Pts',(0.144616374271065,1.02019533918288,1.55063342492034));
#22143=CARTESIAN_POINT('Ctrl Pts',(0.191296207407388,1.01186749890558,1.49078060863542));
#22144=CARTESIAN_POINT('Ctrl Pts',(0.205,1.00876197310684,1.42860317864595));
#22145=CARTESIAN_POINT('Ctrl Pts',(0.205,1.00876197310684,1.4));
#22146=CARTESIAN_POINT('Origin',(0.,1.3,1.4));
#22147=CARTESIAN_POINT('',(0.000131092032552791,1.57001173019275,1.19489555472783));
#22148=CARTESIAN_POINT('',(-2.51052593825207E-17,1.3,1.195));
#22149=CARTESIAN_POINT('',(-0.205,1.55681284340656,1.4));
#22150=CARTESIAN_POINT('Ctrl Pts',(-0.205,1.55681284340656,1.4));
#22151=CARTESIAN_POINT('Ctrl Pts',(-0.205,1.55681284340656,1.36999095977411));
#22152=CARTESIAN_POINT('Ctrl Pts',(-0.189388171591284,1.55880764860196,
1.30517776395932));
#22153=CARTESIAN_POINT('Ctrl Pts',(-0.131226834866621,1.56517193552246,
1.23336580368775));
#22154=CARTESIAN_POINT('Ctrl Pts',(-0.0588701281878798,1.56936404629955,
1.19995504443905));
#22155=CARTESIAN_POINT('Ctrl Pts',(-0.0146362597178014,1.5700109088422,
1.19488207104102));
#22156=CARTESIAN_POINT('Ctrl Pts',(0.000131092032552795,1.57001173019275,
1.19489555472783));
#22157=CARTESIAN_POINT('Ctrl Pts',(0.000131092032552795,1.57001173019275,
1.19489555472783));
#22158=CARTESIAN_POINT('Ctrl Pts',(0.014898443782907,1.57001255154331,1.19490903841464));
#22159=CARTESIAN_POINT('Ctrl Pts',(0.0592686858149541,1.56937061710401,
1.20006291393354));
#22160=CARTESIAN_POINT('Ctrl Pts',(0.11788137682178,1.56585072182196,1.22787750075822));
#22161=CARTESIAN_POINT('Ctrl Pts',(0.15953730265344,1.56201454198299,1.26923760937899));
#22162=CARTESIAN_POINT('Ctrl Pts',(0.211865794877702,1.55611977186479,1.34957830861567));
#22163=CARTESIAN_POINT('Ctrl Pts',(0.211750431534509,1.55626070984013,1.45021602420942));
#22164=CARTESIAN_POINT('Ctrl Pts',(0.159496444970874,1.56209212184905,1.53092039588429));
#22165=CARTESIAN_POINT('Ctrl Pts',(0.117816060861919,1.56594151821204,1.57228130294414));
#22166=CARTESIAN_POINT('Ctrl Pts',(0.0442687531132715,1.57029071330042,
1.60696014729065));
#22167=CARTESIAN_POINT('Ctrl Pts',(-0.0441540900742972,1.57022524422482,
1.60664163567999));
#22168=CARTESIAN_POINT('Ctrl Pts',(-0.131461869516863,1.56518094711964,
1.56655738881618));
#22169=CARTESIAN_POINT('Ctrl Pts',(-0.189333853997008,1.55881441935392,
1.49480011859911));
#22170=CARTESIAN_POINT('Ctrl Pts',(-0.205,1.55681284340656,1.43000904022589));
#22171=CARTESIAN_POINT('Ctrl Pts',(-0.205,1.55681284340656,1.4));
#22172=CARTESIAN_POINT('Origin',(3.985,1.84,0.4));
#22173=CARTESIAN_POINT('',(3.985,1.84,0.0250000000000001));
#22174=CARTESIAN_POINT('',(4.,1.855,0.04));
#22175=CARTESIAN_POINT('',(3.48916666666666,1.34416666666665,-0.470833333333338));
#22176=CARTESIAN_POINT('',(4.,1.855,0.71));
#22177=CARTESIAN_POINT('',(4.,1.855,0.4));
#22178=CARTESIAN_POINT('',(3.98242640687119,1.83742640687119,0.752426406871192));
#22179=CARTESIAN_POINT('',(3.77907310450642,1.63407310450642,1.24336470739356));
#22180=CARTESIAN_POINT('',(3.97,1.825,0.74));
#22181=CARTESIAN_POINT('',(3.44166666666668,1.29666666666667,0.21166666666667));
#22182=CARTESIAN_POINT('',(3.97,1.825,0.04));
#22183=CARTESIAN_POINT('',(3.97,1.825,0.4));
#22184=CARTESIAN_POINT('',(3.43500000000002,1.29,0.574999999999997));
#22185=CARTESIAN_POINT('Origin',(2.1,1.825,0.8));
#22186=CARTESIAN_POINT('',(2.1,1.825,0.74));
#22187=CARTESIAN_POINT('',(1.05,1.825,0.74));
#22188=CARTESIAN_POINT('',(2.1,1.825,0.04));
#22189=CARTESIAN_POINT('',(2.1,1.825,0.8));
#22190=CARTESIAN_POINT('',(1.05,1.825,0.04));
#22191=CARTESIAN_POINT('Origin',(1.05,1.855,0.77));
#22192=CARTESIAN_POINT('',(3.9787867965644,1.8462132034356,0.761213203435596));
#22193=CARTESIAN_POINT('',(4.25493545624507,1.17953136400341,0.094531364003406));
#22194=CARTESIAN_POINT('',(3.9612132034356,1.8637867965644,0.778786796564404));
#22195=CARTESIAN_POINT('',(3.94,1.885,0.8));
#22196=CARTESIAN_POINT('',(2.1,1.8637867965644,0.778786796564404));
#22197=CARTESIAN_POINT('',(0.525,1.8637867965644,0.778786796564404));
#22198=CARTESIAN_POINT('',(2.1,1.825,0.74));
#22199=CARTESIAN_POINT('Origin',(3.9893933982822,-2.25,0.735606601717798));
#22200=CARTESIAN_POINT('',(4.,2.6,0.71));
#22201=CARTESIAN_POINT('',(4.,-2.25,0.71));
#22202=CARTESIAN_POINT('',(3.9787867965644,2.6,0.761213203435597));
#22203=CARTESIAN_POINT('',(4.,2.6,0.71));
#22204=CARTESIAN_POINT('',(3.9787867965644,-2.25,0.761213203435596));
#22205=CARTESIAN_POINT('Origin',(-3.985,1.84,0.4));
#22206=CARTESIAN_POINT('',(-3.98242640687119,1.83742640687119,0.752426406871192));
#22207=CARTESIAN_POINT('',(-4.,1.855,0.71));
#22208=CARTESIAN_POINT('',(-4.06648716152533,1.92148716152533,0.549485792921871));
#22209=CARTESIAN_POINT('',(-4.,1.855,0.04));
#22210=CARTESIAN_POINT('',(-4.,1.855,0.4));
#22211=CARTESIAN_POINT('',(-3.985,1.84,0.0250000000000002));
#22212=CARTESIAN_POINT('',(-3.98916666666666,1.84416666666666,0.029166666666665));
#22213=CARTESIAN_POINT('',(-3.97,1.825,0.04));
#22214=CARTESIAN_POINT('',(-3.60166666666668,1.45666666666667,0.408333333333331));
#22215=CARTESIAN_POINT('',(-3.97,1.825,0.74));
#22216=CARTESIAN_POINT('',(-3.97,1.825,0.4));
#22217=CARTESIAN_POINT('',(-3.60833333333335,1.46333333333334,0.378333333333335));
#22218=CARTESIAN_POINT('Origin',(-3.98,1.5,0.02));
#22219=CARTESIAN_POINT('',(-4.,2.6,0.04));
#22220=CARTESIAN_POINT('',(-4.,1.5,0.04));
#22221=CARTESIAN_POINT('',(-3.96,2.6,0.));
#22222=CARTESIAN_POINT('',(-3.96,2.6,0.));
#22223=CARTESIAN_POINT('',(-3.96,1.865,0.));
#22224=CARTESIAN_POINT('',(-3.96,1.5,0.));
#22225=CARTESIAN_POINT('',(-3.96,1.865,0.));
#22226=CARTESIAN_POINT('Origin',(-4.,3.,0.));
#22227=CARTESIAN_POINT('',(-4.,2.6,0.71));
#22228=CARTESIAN_POINT('',(-4.,2.25,0.71));
#22229=CARTESIAN_POINT('',(-4.,2.6,0.));
#22230=CARTESIAN_POINT('Origin',(-3.9893933982822,2.25,0.735606601717798));
#22231=CARTESIAN_POINT('',(-3.9787867965644,1.8462132034356,0.761213203435597));
#22232=CARTESIAN_POINT('',(-3.86526671090596,2.12027493383395,1.03527493383395));
#22233=CARTESIAN_POINT('',(-3.9787867965644,2.6,0.761213203435597));
#22234=CARTESIAN_POINT('',(-3.9787867965644,2.25,0.761213203435596));
#22235=CARTESIAN_POINT('',(-4.,2.6,0.71));
#22236=CARTESIAN_POINT('Origin',(3.6,2.6,0.735606601717798));
#22237=CARTESIAN_POINT('',(3.6,3.,0.71));
#22238=CARTESIAN_POINT('',(3.6,2.9787867965644,0.761213203435597));
#22239=CARTESIAN_POINT('',(3.6,3.,0.71));
#22240=CARTESIAN_POINT('Origin',(3.6,2.6,0.761213203435597));
#22241=CARTESIAN_POINT('Origin',(3.6,2.6,0.71));
#22242=CARTESIAN_POINT('Origin',(3.,2.9893933982822,0.735606601717798));
#22243=CARTESIAN_POINT('',(-3.6,3.,0.71));
#22244=CARTESIAN_POINT('',(-3.6,2.9787867965644,0.761213203435597));
#22245=CARTESIAN_POINT('',(-3.6,3.,0.71));
#22246=CARTESIAN_POINT('',(3.,2.9787867965644,0.761213203435596));
#22247=CARTESIAN_POINT('',(3.,3.,0.71));
#22248=CARTESIAN_POINT('Origin',(-3.6,2.6,0.735606601717798));
#22249=CARTESIAN_POINT('Origin',(-3.6,2.6,0.761213203435597));
#22250=CARTESIAN_POINT('Origin',(-3.6,2.6,0.71));
#22251=CARTESIAN_POINT('Origin',(-2.05,1.855,0.77));
#22252=CARTESIAN_POINT('',(-2.1,1.825,0.74));
#22253=CARTESIAN_POINT('',(-2.05,1.825,0.74));
#22254=CARTESIAN_POINT('',(-2.1,1.8637867965644,0.778786796564404));
#22255=CARTESIAN_POINT('',(-2.1,1.825,0.74));
#22256=CARTESIAN_POINT('',(-3.9612132034356,1.8637867965644,0.778786796564404));
#22257=CARTESIAN_POINT('',(-1.025,1.8637867965644,0.778786796564404));
#22258=CARTESIAN_POINT('',(-3.94,1.885,0.8));
#22259=CARTESIAN_POINT('Origin',(-4.1,1.825,0.8));
#22260=CARTESIAN_POINT('',(-2.1,1.825,0.04));
#22261=CARTESIAN_POINT('',(-2.05,1.825,0.04));
#22262=CARTESIAN_POINT('',(-2.1,1.825,0.8));
#22263=CARTESIAN_POINT('Origin',(-3.6,2.6,0.));
#22264=CARTESIAN_POINT('',(-3.6,3.,0.04));
#22265=CARTESIAN_POINT('',(-3.6,3.,0.));
#22266=CARTESIAN_POINT('Origin',(-3.6,2.6,0.04));
#22267=CARTESIAN_POINT('Origin',(4.,3.,0.));
#22268=CARTESIAN_POINT('',(3.6,3.,0.04));
#22269=CARTESIAN_POINT('',(3.6,3.,0.));
#22270=CARTESIAN_POINT('',(2.,3.,0.04));
#22271=CARTESIAN_POINT('Origin',(3.6,2.6,0.));
#22272=CARTESIAN_POINT('',(4.,2.6,0.04));
#22273=CARTESIAN_POINT('',(4.,2.6,0.));
#22274=CARTESIAN_POINT('Origin',(3.6,2.6,0.04));
#22275=CARTESIAN_POINT('Origin',(4.,-3.,0.));
#22276=CARTESIAN_POINT('',(4.,-1.5,0.04));
#22277=CARTESIAN_POINT('Origin',(-3.9356066017178,0.75,0.789393398282202));
#22278=CARTESIAN_POINT('',(-3.91,1.915,0.8));
#22279=CARTESIAN_POINT('',(-3.52778855802712,2.29721144197289,0.958317162959347));
#22280=CARTESIAN_POINT('',(-3.91,2.6,0.8));
#22281=CARTESIAN_POINT('',(-3.91,0.75,0.8));
#22282=CARTESIAN_POINT('',(-3.9612132034356,2.6,0.778786796564403));
#22283=CARTESIAN_POINT('',(-3.91,2.6,0.8));
#22284=CARTESIAN_POINT('',(-3.9612132034356,0.75,0.778786796564403));
#22285=CARTESIAN_POINT('Origin',(-3.6,2.6,0.789393398282202));
#22286=CARTESIAN_POINT('',(-3.6,2.91,0.8));
#22287=CARTESIAN_POINT('',(-3.6,2.9612132034356,0.778786796564404));
#22288=CARTESIAN_POINT('',(-3.6,2.91,0.8));
#22289=CARTESIAN_POINT('Origin',(-3.6,2.6,0.778786796564404));
#22290=CARTESIAN_POINT('Origin',(-3.6,2.6,0.8));
#22291=CARTESIAN_POINT('Origin',(1.,2.9356066017178,0.789393398282202));
#22292=CARTESIAN_POINT('',(3.6,2.91,0.8));
#22293=CARTESIAN_POINT('',(3.6,2.9612132034356,0.778786796564403));
#22294=CARTESIAN_POINT('',(3.6,2.91,0.8));
#22295=CARTESIAN_POINT('',(1.,2.9612132034356,0.778786796564403));
#22296=CARTESIAN_POINT('',(1.,2.91,0.8));
#22297=CARTESIAN_POINT('Origin',(3.6,2.6,0.789393398282202));
#22298=CARTESIAN_POINT('',(3.91,2.6,0.8));
#22299=CARTESIAN_POINT('',(3.9612132034356,2.6,0.778786796564404));
#22300=CARTESIAN_POINT('',(3.91,2.6,0.8));
#22301=CARTESIAN_POINT('Origin',(3.6,2.6,0.778786796564404));
#22302=CARTESIAN_POINT('Origin',(3.6,2.6,0.8));
#22303=CARTESIAN_POINT('Origin',(3.9356066017178,-0.75,0.789393398282202));
#22304=CARTESIAN_POINT('',(3.91,1.915,0.8));
#22305=CARTESIAN_POINT('',(3.75803641463731,2.0669635853627,0.86294537804407));
#22306=CARTESIAN_POINT('',(3.9612132034356,-0.75,0.778786796564403));
#22307=CARTESIAN_POINT('',(3.91,-0.75,0.8));
#22308=CARTESIAN_POINT('Origin',(-3.97,1.5,0.77));
#22309=CARTESIAN_POINT('',(-4.,2.6,0.74));
#22310=CARTESIAN_POINT('Origin',(-3.6,2.6,0.77));
#22311=CARTESIAN_POINT('',(-3.6,3.,0.74));
#22312=CARTESIAN_POINT('Origin',(2.,2.97,0.77));
#22313=CARTESIAN_POINT('',(3.6,3.,0.74));
#22314=CARTESIAN_POINT('Origin',(3.6,2.6,0.77));
#22315=CARTESIAN_POINT('',(4.,2.6,0.74));
#22316=CARTESIAN_POINT('Origin',(3.97,-1.5,0.77));
#22317=CARTESIAN_POINT('Origin',(0.525,1.8893933982822,0.789393398282202));
#22318=CARTESIAN_POINT('',(2.1,1.915,0.8));
#22319=CARTESIAN_POINT('',(0.525,1.915,0.8));
#22320=CARTESIAN_POINT('',(2.1,1.915,0.8));
#22321=CARTESIAN_POINT('Origin',(2.1,1.5,0.789393398282202));
#22322=CARTESIAN_POINT('',(2.1,1.085,0.8));
#22323=CARTESIAN_POINT('',(2.1,1.085,0.8));
#22324=CARTESIAN_POINT('Origin',(2.1,1.5,0.778786796564404));
#22325=CARTESIAN_POINT('Origin',(2.1,1.5,0.8));
#22326=CARTESIAN_POINT('Origin',(1.025,1.1106066017178,0.789393398282202));
#22327=CARTESIAN_POINT('',(3.91,1.085,0.8));
#22328=CARTESIAN_POINT('',(1.025,1.085,0.8));
#22329=CARTESIAN_POINT('',(3.91,1.085,0.8));
#22330=CARTESIAN_POINT('Origin',(3.9356066017178,-0.75,0.789393398282202));
#22331=CARTESIAN_POINT('',(3.91,-1.085,0.8));
#22332=CARTESIAN_POINT('',(3.91,-0.75,0.8));
#22333=CARTESIAN_POINT('',(3.91,-1.085,0.8));
#22334=CARTESIAN_POINT('Origin',(0.525,-1.1106066017178,0.789393398282202));
#22335=CARTESIAN_POINT('',(2.1,-1.085,0.8));
#22336=CARTESIAN_POINT('',(0.525,-1.085,0.8));
#22337=CARTESIAN_POINT('',(2.1,-1.085,0.8));
#22338=CARTESIAN_POINT('Origin',(2.1,-1.5,0.789393398282202));
#22339=CARTESIAN_POINT('',(2.1,-1.915,0.8));
#22340=CARTESIAN_POINT('',(2.1,-1.915,0.8));
#22341=CARTESIAN_POINT('Origin',(2.1,-1.5,0.778786796564404));
#22342=CARTESIAN_POINT('Origin',(2.1,-1.5,0.8));
#22343=CARTESIAN_POINT('Origin',(1.025,-1.8893933982822,0.789393398282202));
#22344=CARTESIAN_POINT('',(3.91,-1.915,0.8));
#22345=CARTESIAN_POINT('',(1.025,-1.915,0.8));
#22346=CARTESIAN_POINT('',(3.91,-1.915,0.8));
#22347=CARTESIAN_POINT('Origin',(3.9356066017178,-0.75,0.789393398282202));
#22348=CARTESIAN_POINT('',(3.91,-2.6,0.8));
#22349=CARTESIAN_POINT('',(3.91,-0.75,0.8));
#22350=CARTESIAN_POINT('',(3.91,-2.6,0.8));
#22351=CARTESIAN_POINT('Origin',(3.6,-2.6,0.789393398282202));
#22352=CARTESIAN_POINT('',(3.6,-2.91,0.8));
#22353=CARTESIAN_POINT('',(3.6,-2.9612132034356,0.778786796564404));
#22354=CARTESIAN_POINT('',(3.6,-2.91,0.8));
#22355=CARTESIAN_POINT('Origin',(3.6,-2.6,0.778786796564404));
#22356=CARTESIAN_POINT('Origin',(3.6,-2.6,0.8));
#22357=CARTESIAN_POINT('Origin',(-1.,-2.9356066017178,0.789393398282202));
#22358=CARTESIAN_POINT('',(-3.6,-2.91,0.8));
#22359=CARTESIAN_POINT('',(-3.6,-2.9612132034356,0.778786796564403));
#22360=CARTESIAN_POINT('',(-3.6,-2.91,0.8));
#22361=CARTESIAN_POINT('',(-1.,-2.9612132034356,0.778786796564403));
#22362=CARTESIAN_POINT('',(-1.,-2.91,0.8));
#22363=CARTESIAN_POINT('Origin',(-3.6,-2.6,0.789393398282202));
#22364=CARTESIAN_POINT('',(-3.91,-2.6,0.8));
#22365=CARTESIAN_POINT('',(-3.91,-2.6,0.8));
#22366=CARTESIAN_POINT('Origin',(-3.6,-2.6,0.778786796564404));
#22367=CARTESIAN_POINT('Origin',(-3.6,-2.6,0.8));
#22368=CARTESIAN_POINT('Origin',(-3.9356066017178,0.75,0.789393398282202));
#22369=CARTESIAN_POINT('',(-3.91,-1.915,0.8));
#22370=CARTESIAN_POINT('',(-3.91,0.75,0.8));
#22371=CARTESIAN_POINT('',(-3.91,-1.915,0.8));
#22372=CARTESIAN_POINT('Origin',(-0.525,-1.8893933982822,0.789393398282202));
#22373=CARTESIAN_POINT('',(-2.1,-1.915,0.8));
#22374=CARTESIAN_POINT('',(-0.525,-1.915,0.8));
#22375=CARTESIAN_POINT('',(-2.1,-1.8637867965644,0.778786796564404));
#22376=CARTESIAN_POINT('',(-2.1,-1.915,0.8));
#22377=CARTESIAN_POINT('',(-0.525,-1.8637867965644,0.778786796564404));
#22378=CARTESIAN_POINT('Origin',(-2.1,-1.5,0.789393398282202));
#22379=CARTESIAN_POINT('',(-2.1,-1.085,0.8));
#22380=CARTESIAN_POINT('',(-2.1,-1.1362132034356,0.778786796564404));
#22381=CARTESIAN_POINT('',(-2.1,-1.085,0.8));
#22382=CARTESIAN_POINT('Origin',(-2.1,-1.5,0.778786796564404));
#22383=CARTESIAN_POINT('Origin',(-2.1,-1.5,0.8));
#22384=CARTESIAN_POINT('Origin',(-1.025,-1.1106066017178,0.789393398282202));
#22385=CARTESIAN_POINT('',(-1.025,-1.1362132034356,0.778786796564404));
#22386=CARTESIAN_POINT('',(-3.91,-1.085,0.8));
#22387=CARTESIAN_POINT('',(-1.025,-1.085,0.8));
#22388=CARTESIAN_POINT('',(-3.91,-1.085,0.8));
#22389=CARTESIAN_POINT('Origin',(-3.9356066017178,0.75,0.789393398282202));
#22390=CARTESIAN_POINT('',(-3.91,1.085,0.8));
#22391=CARTESIAN_POINT('',(-3.91,0.75,0.8));
#22392=CARTESIAN_POINT('',(-3.91,1.085,0.8));
#22393=CARTESIAN_POINT('Origin',(-0.525,1.1106066017178,0.789393398282202));
#22394=CARTESIAN_POINT('',(-2.1,1.085,0.8));
#22395=CARTESIAN_POINT('',(-0.525,1.085,0.8));
#22396=CARTESIAN_POINT('',(-2.1,1.1362132034356,0.778786796564404));
#22397=CARTESIAN_POINT('',(-2.1,1.085,0.8));
#22398=CARTESIAN_POINT('',(-0.525,1.1362132034356,0.778786796564404));
#22399=CARTESIAN_POINT('Origin',(-2.1,1.5,0.789393398282202));
#22400=CARTESIAN_POINT('',(-2.1,1.915,0.8));
#22401=CARTESIAN_POINT('',(-2.1,1.915,0.8));
#22402=CARTESIAN_POINT('Origin',(-2.1,1.5,0.778786796564404));
#22403=CARTESIAN_POINT('Origin',(-2.1,1.5,0.8));
#22404=CARTESIAN_POINT('Origin',(-1.025,1.8893933982822,0.789393398282202));
#22405=CARTESIAN_POINT('',(-1.025,1.915,0.8));
#22406=CARTESIAN_POINT('Origin',(0.,0.,0.8));
#22407=CARTESIAN_POINT('',(1.75,-2.14313189850787E-16,0.8));
#22408=CARTESIAN_POINT('Origin',(0.,0.,0.8));
#22409=CARTESIAN_POINT('Ctrl Pts',(-0.2347153981354,1.58269033037993,1.4));
#22410=CARTESIAN_POINT('Ctrl Pts',(-0.2347153981354,1.58269033037993,1.36620206917426));
#22411=CARTESIAN_POINT('Ctrl Pts',(-0.217558446824302,1.5852549399837,1.29316877041114));
#22412=CARTESIAN_POINT('Ctrl Pts',(-0.152415457266674,1.59355456054094,
1.21049566567658));
#22413=CARTESIAN_POINT('Ctrl Pts',(-0.0521025187876913,1.6002700877622,
1.1629600177189));
#22414=CARTESIAN_POINT('Ctrl Pts',(0.0523288394347715,1.60033288629179,
1.1627635323513));
#22415=CARTESIAN_POINT('Ctrl Pts',(0.136901297650221,1.5944726374199,1.20393468493575));
#22416=CARTESIAN_POINT('Ctrl Pts',(0.184075177725469,1.58943902120323,1.2517856376839));
#22417=CARTESIAN_POINT('Ctrl Pts',(0.242438373304523,1.58178434531461,1.3436546039934));
#22418=CARTESIAN_POINT('Ctrl Pts',(0.242424895429431,1.58195751401911,1.45610993307891));
#22419=CARTESIAN_POINT('Ctrl Pts',(0.184096357151629,1.58953393073711,1.54838937357335));
#22420=CARTESIAN_POINT('Ctrl Pts',(0.136902935945947,1.59458452325023,1.59624390388577));
#22421=CARTESIAN_POINT('Ctrl Pts',(0.0519568849441468,1.60038159630494,
1.63731023393358));
#22422=CARTESIAN_POINT('Ctrl Pts',(-0.0517911204160937,1.60029839497895,
1.63694413004937));
#22423=CARTESIAN_POINT('Ctrl Pts',(-0.152692584771416,1.59356568559404,
1.58941995958521));
#22424=CARTESIAN_POINT('Ctrl Pts',(-0.217487941313751,1.58526334196631,
1.50680645542181));
#22425=CARTESIAN_POINT('Ctrl Pts',(-0.2347153981354,1.58269033037993,1.43379793082574));
#22426=CARTESIAN_POINT('Ctrl Pts',(-0.2347153981354,1.58269033037993,1.4));
#22427=CARTESIAN_POINT('Ctrl Pts',(-0.2248102654236,1.57406450138881,1.4));
#22428=CARTESIAN_POINT('Ctrl Pts',(-0.2248102654236,1.57406450138881,1.36746503270754));
#22429=CARTESIAN_POINT('Ctrl Pts',(-0.208168355079963,1.57643917618978,
1.29717176826053));
#22430=CARTESIAN_POINT('Ctrl Pts',(-0.145352583133322,1.58409368553478,
1.21811904501364));
#22431=CARTESIAN_POINT('Ctrl Pts',(-0.0495346081425047,1.59024754799312,
1.17306430934237));
#22432=CARTESIAN_POINT('Ctrl Pts',(0.0497577306442636,1.5903054545027,1.17287877730999));
#22433=CARTESIAN_POINT('Ctrl Pts',(0.13056132404074,1.58493199888725,1.21191562354324));
#22434=CARTESIAN_POINT('Ctrl Pts',(0.175895886034792,1.58029752812982,1.25760296158226));
#22435=CARTESIAN_POINT('Ctrl Pts',(0.232247513828916,1.573229487498,1.34562917220083));
#22436=CARTESIAN_POINT('Ctrl Pts',(0.232200074131124,1.57339191262612,1.45414529678908));
#22437=CARTESIAN_POINT('Ctrl Pts',(0.17589638642471,1.58038666110775,1.54256638101033));
#22438=CARTESIAN_POINT('Ctrl Pts',(0.130540644251271,1.58503685490416,1.58825637023856));
#22439=CARTESIAN_POINT('Ctrl Pts',(0.049394174333855,1.5903513019701,1.62719353838594));
#22440=CARTESIAN_POINT('Ctrl Pts',(-0.049245443635495,1.59027401139424,
1.62684329859291));
#22441=CARTESIAN_POINT('Ctrl Pts',(-0.145615679686565,1.58410410610257,
1.5817991026622));
#22442=CARTESIAN_POINT('Ctrl Pts',(-0.208103245541503,1.57644703442885,
1.50280434314757));
#22443=CARTESIAN_POINT('Ctrl Pts',(-0.2248102654236,1.57406450138881,1.43253496729245));
#22444=CARTESIAN_POINT('Ctrl Pts',(-0.2248102654236,1.57406450138881,1.4));
#22445=CARTESIAN_POINT('Ctrl Pts',(-0.2149051327118,1.56543867239768,1.4));
#22446=CARTESIAN_POINT('Ctrl Pts',(-0.2149051327118,1.56543867239768,1.36872799624083));
#22447=CARTESIAN_POINT('Ctrl Pts',(-0.198778263335623,1.56762341239587,
1.30117476610993));
#22448=CARTESIAN_POINT('Ctrl Pts',(-0.138289708999972,1.57463281052862,
1.22574242435069));
#22449=CARTESIAN_POINT('Ctrl Pts',(-0.0469666974973182,1.58022500822404,
1.18316860096584));
#22450=CARTESIAN_POINT('Ctrl Pts',(0.0471866218537556,1.58027802271362,
1.18299402226868));
#22451=CARTESIAN_POINT('Ctrl Pts',(0.12422135043126,1.5753913603546,1.21989656215073));
#22452=CARTESIAN_POINT('Ctrl Pts',(0.167716594344116,1.57115603505641,1.26342028548062));
#22453=CARTESIAN_POINT('Ctrl Pts',(0.222056654353309,1.5646746296814,1.34760374040825));
#22454=CARTESIAN_POINT('Ctrl Pts',(0.221975252832816,1.56482631123312,1.45218066049925));
#22455=CARTESIAN_POINT('Ctrl Pts',(0.167696415697792,1.5712393914784,1.53674338844731));
#22456=CARTESIAN_POINT('Ctrl Pts',(0.124178352556595,1.5754891865581,1.58026883659135));
#22457=CARTESIAN_POINT('Ctrl Pts',(0.0468314637235632,1.58032100763526,
1.61707684283829));
#22458=CARTESIAN_POINT('Ctrl Pts',(-0.0466997668548959,1.58024962780953,
1.61674246713645));
#22459=CARTESIAN_POINT('Ctrl Pts',(-0.138538774601714,1.57464252661111,
1.57417824573919));
#22460=CARTESIAN_POINT('Ctrl Pts',(-0.198718549769256,1.56763072689139,
1.49880223087334));
#22461=CARTESIAN_POINT('Ctrl Pts',(-0.2149051327118,1.56543867239768,1.43127200375917));
#22462=CARTESIAN_POINT('Ctrl Pts',(-0.2149051327118,1.56543867239768,1.4));
#22463=CARTESIAN_POINT('Ctrl Pts',(-0.205,1.55681284340656,1.4));
#22464=CARTESIAN_POINT('Ctrl Pts',(-0.205,1.55681284340656,1.36999095977411));
#22465=CARTESIAN_POINT('Ctrl Pts',(-0.189388171591284,1.55880764860196,
1.30517776395932));
#22466=CARTESIAN_POINT('Ctrl Pts',(-0.131226834866621,1.56517193552246,
1.23336580368775));
#22467=CARTESIAN_POINT('Ctrl Pts',(-0.0443987868521316,1.57020246845496,
1.19327289258931));
#22468=CARTESIAN_POINT('Ctrl Pts',(0.0446155130632477,1.57025059092453,
1.19310926722737));
#22469=CARTESIAN_POINT('Ctrl Pts',(0.11788137682178,1.56585072182196,1.22787750075822));
#22470=CARTESIAN_POINT('Ctrl Pts',(0.15953730265344,1.56201454198299,1.26923760937899));
#22471=CARTESIAN_POINT('Ctrl Pts',(0.211865794877702,1.55611977186479,1.34957830861567));
#22472=CARTESIAN_POINT('Ctrl Pts',(0.211750431534509,1.55626070984013,1.45021602420942));
#22473=CARTESIAN_POINT('Ctrl Pts',(0.159496444970874,1.56209212184905,1.53092039588429));
#22474=CARTESIAN_POINT('Ctrl Pts',(0.117816060861919,1.56594151821204,1.57228130294414));
#22475=CARTESIAN_POINT('Ctrl Pts',(0.0442687531132715,1.57029071330042,
1.60696014729065));
#22476=CARTESIAN_POINT('Ctrl Pts',(-0.0441540900742972,1.57022524422482,
1.60664163567999));
#22477=CARTESIAN_POINT('Ctrl Pts',(-0.131461869516863,1.56518094711964,
1.56655738881618));
#22478=CARTESIAN_POINT('Ctrl Pts',(-0.189333853997008,1.55881441935392,
1.49480011859911));
#22479=CARTESIAN_POINT('Ctrl Pts',(-0.205,1.55681284340656,1.43000904022589));
#22480=CARTESIAN_POINT('Ctrl Pts',(-0.205,1.55681284340656,1.4));
#22481=CARTESIAN_POINT('',(-0.2347153981354,1.58269033037993,1.4));
#22482=CARTESIAN_POINT('',(-0.2347153981354,1.58269033037993,1.4));
#22483=CARTESIAN_POINT('Ctrl Pts',(-0.2347153981354,1.58269033037993,1.4));
#22484=CARTESIAN_POINT('Ctrl Pts',(-0.2347153981354,1.58269033037993,1.43379793082574));
#22485=CARTESIAN_POINT('Ctrl Pts',(-0.217487941313751,1.58526334196631,
1.50680645542181));
#22486=CARTESIAN_POINT('Ctrl Pts',(-0.152692584771416,1.59356568559404,
1.58941995958521));
#22487=CARTESIAN_POINT('Ctrl Pts',(-0.0517911204160937,1.60029839497895,
1.63694413004937));
#22488=CARTESIAN_POINT('Ctrl Pts',(0.0519568849441468,1.60038159630494,
1.63731023393358));
#22489=CARTESIAN_POINT('Ctrl Pts',(0.136902935945947,1.59458452325023,1.59624390388577));
#22490=CARTESIAN_POINT('Ctrl Pts',(0.184096357151629,1.58953393073711,1.54838937357335));
#22491=CARTESIAN_POINT('Ctrl Pts',(0.242424895429431,1.58195751401911,1.45610993307891));
#22492=CARTESIAN_POINT('Ctrl Pts',(0.242438373304523,1.58178434531461,1.3436546039934));
#22493=CARTESIAN_POINT('Ctrl Pts',(0.184075177725469,1.58943902120323,1.2517856376839));
#22494=CARTESIAN_POINT('Ctrl Pts',(0.136901297650221,1.5944726374199,1.20393468493575));
#22495=CARTESIAN_POINT('Ctrl Pts',(0.0523288394347715,1.60033288629179,
1.1627635323513));
#22496=CARTESIAN_POINT('Ctrl Pts',(-0.0521025187876913,1.6002700877622,
1.1629600177189));
#22497=CARTESIAN_POINT('Ctrl Pts',(-0.152415457266674,1.59355456054094,
1.21049566567658));
#22498=CARTESIAN_POINT('Ctrl Pts',(-0.217558446824302,1.5852549399837,1.29316877041114));
#22499=CARTESIAN_POINT('Ctrl Pts',(-0.2347153981354,1.58269033037993,1.36620206917426));
#22500=CARTESIAN_POINT('Ctrl Pts',(-0.2347153981354,1.58269033037993,1.4));
#22501=CARTESIAN_POINT('Origin',(0.,0.,0.8));
#22502=CARTESIAN_POINT('',(-1.6,-1.95943487863577E-16,1.91));
#22503=CARTESIAN_POINT('Origin',(0.,0.,1.91));
#22504=CARTESIAN_POINT('',(-1.6,1.95943487863577E-16,0.95));
#22505=CARTESIAN_POINT('',(-1.6,-1.95943487863577E-16,0.8));
#22506=CARTESIAN_POINT('',(1.6,-1.95943487863577E-16,0.95));
#22507=CARTESIAN_POINT('Origin',(0.,0.,0.95));
#22508=CARTESIAN_POINT('Origin',(0.,0.,0.95));
#22509=CARTESIAN_POINT('Origin',(0.,-4.83364049237175E-17,1.9356066017178));
#22510=CARTESIAN_POINT('',(-1.5787867965644,0.,1.9612132034356));
#22511=CARTESIAN_POINT('Origin',(0.,-9.6672809847435E-17,1.9612132034356));
#22512=CARTESIAN_POINT('',(-1.5893933982822,-2.91317363626658E-16,1.9356066017178));
#22513=CARTESIAN_POINT('Origin',(0.,0.,1.97));
#22514=CARTESIAN_POINT('',(-1.57,-1.92269547466134E-16,1.97));
#22515=CARTESIAN_POINT('Origin',(0.,0.,0.95));
#22516=CARTESIAN_POINT('Origin',(1.75,-2.14313189850787E-16,0.95));
#22517=CARTESIAN_POINT('Origin',(0.,0.,0.4));
#22518=CARTESIAN_POINT('Origin',(3.98,-1.5,0.02));
#22519=CARTESIAN_POINT('',(3.96,1.865,0.));
#22520=CARTESIAN_POINT('',(4.,1.825,0.04));
#22521=CARTESIAN_POINT('',(3.96,2.6,0.));
#22522=CARTESIAN_POINT('',(3.96,-1.5,0.));
#22523=CARTESIAN_POINT('',(3.96,2.6,0.));
#22524=CARTESIAN_POINT('Origin',(3.98,-1.5,0.02));
#22525=CARTESIAN_POINT('',(3.96,-1.135,0.));
#22526=CARTESIAN_POINT('',(4.,-1.175,0.04));
#22527=CARTESIAN_POINT('',(3.96,1.135,0.));
#22528=CARTESIAN_POINT('',(3.96,-1.5,0.));
#22529=CARTESIAN_POINT('',(3.96,1.135,0.));
#22530=CARTESIAN_POINT('Origin',(-3.6,-2.6,0.02));
#22531=CARTESIAN_POINT('',(-3.6,-2.96,0.));
#22532=CARTESIAN_POINT('',(-3.6,-3.,0.04));
#22533=CARTESIAN_POINT('',(-3.6,-2.96,0.));
#22534=CARTESIAN_POINT('Origin',(-3.6,-2.6,0.04));
#22535=CARTESIAN_POINT('Origin',(-3.6,-2.6,0.));
#22536=CARTESIAN_POINT('Origin',(-2.,-2.98,0.02));
#22537=CARTESIAN_POINT('',(3.6,-2.96,0.));
#22538=CARTESIAN_POINT('',(3.6,-3.,0.04));
#22539=CARTESIAN_POINT('',(3.6,-2.96,0.));
#22540=CARTESIAN_POINT('',(-2.,-3.,0.04));
#22541=CARTESIAN_POINT('',(-2.,-2.96,0.));
#22542=CARTESIAN_POINT('Origin',(3.6,-2.6,0.02));
#22543=CARTESIAN_POINT('',(3.96,-2.6,0.));
#22544=CARTESIAN_POINT('',(3.96,-2.6,0.));
#22545=CARTESIAN_POINT('Origin',(3.6,-2.6,0.04));
#22546=CARTESIAN_POINT('Origin',(3.6,-2.6,0.));
#22547=CARTESIAN_POINT('Origin',(3.98,-1.5,0.02));
#22548=CARTESIAN_POINT('',(3.96,-1.865,0.));
#22549=CARTESIAN_POINT('',(3.96,-1.5,0.));
#22550=CARTESIAN_POINT('',(3.96,-1.865,0.));
#22551=CARTESIAN_POINT('Origin',(-1.05,-1.845,0.02));
#22552=CARTESIAN_POINT('',(-2.1,-1.825,0.04));
#22553=CARTESIAN_POINT('',(-1.05,-1.825,0.04));
#22554=CARTESIAN_POINT('',(-2.1,-1.865,0.));
#22555=CARTESIAN_POINT('',(-2.1,-1.825,0.04));
#22556=CARTESIAN_POINT('',(-1.05,-1.865,0.));
#22557=CARTESIAN_POINT('Origin',(-2.1,-1.5,0.02));
#22558=CARTESIAN_POINT('',(-2.1,-1.175,0.04));
#22559=CARTESIAN_POINT('',(-2.1,-1.135,0.));
#22560=CARTESIAN_POINT('',(-2.1,-1.175,0.04));
#22561=CARTESIAN_POINT('Origin',(-2.1,-1.5,0.));
#22562=CARTESIAN_POINT('Origin',(-2.1,-1.5,0.04));
#22563=CARTESIAN_POINT('Origin',(-2.05,-1.155,0.02));
#22564=CARTESIAN_POINT('',(-2.05,-1.135,0.));
#22565=CARTESIAN_POINT('',(-2.05,-1.175,0.04));
#22566=CARTESIAN_POINT('Origin',(1.05,-1.155,0.02));
#22567=CARTESIAN_POINT('',(2.1,-1.175,0.04));
#22568=CARTESIAN_POINT('',(1.05,-1.175,0.04));
#22569=CARTESIAN_POINT('',(2.1,-1.135,0.));
#22570=CARTESIAN_POINT('',(2.1,-1.175,0.04));
#22571=CARTESIAN_POINT('',(1.05,-1.135,0.));
#22572=CARTESIAN_POINT('Origin',(2.1,-1.5,0.02));
#22573=CARTESIAN_POINT('',(2.1,-1.825,0.04));
#22574=CARTESIAN_POINT('',(2.1,-1.865,0.));
#22575=CARTESIAN_POINT('',(2.1,-1.825,0.04));
#22576=CARTESIAN_POINT('Origin',(2.1,-1.5,0.));
#22577=CARTESIAN_POINT('Origin',(2.1,-1.5,0.04));
#22578=CARTESIAN_POINT('Origin',(2.05,-1.845,0.02));
#22579=CARTESIAN_POINT('',(2.05,-1.865,0.));
#22580=CARTESIAN_POINT('',(2.05,-1.825,0.04));
#22581=CARTESIAN_POINT('Origin',(-1.05,1.155,0.02));
#22582=CARTESIAN_POINT('',(-2.1,1.175,0.04));
#22583=CARTESIAN_POINT('',(-1.05,1.175,0.04));
#22584=CARTESIAN_POINT('',(-2.1,1.135,0.));
#22585=CARTESIAN_POINT('',(-2.1,1.175,0.04));
#22586=CARTESIAN_POINT('',(-1.05,1.135,0.));
#22587=CARTESIAN_POINT('Origin',(-2.1,1.5,0.02));
#22588=CARTESIAN_POINT('',(-2.1,1.865,0.));
#22589=CARTESIAN_POINT('',(-2.1,1.825,0.04));
#22590=CARTESIAN_POINT('Origin',(-2.1,1.5,0.));
#22591=CARTESIAN_POINT('Origin',(-2.1,1.5,0.04));
#22592=CARTESIAN_POINT('Origin',(-2.05,1.845,0.02));
#22593=CARTESIAN_POINT('',(-2.05,1.865,0.));
#22594=CARTESIAN_POINT('Origin',(1.05,1.845,0.02));
#22595=CARTESIAN_POINT('',(2.1,1.865,0.));
#22596=CARTESIAN_POINT('',(2.1,1.825,0.04));
#22597=CARTESIAN_POINT('',(1.05,1.865,0.));
#22598=CARTESIAN_POINT('Origin',(2.1,1.5,0.02));
#22599=CARTESIAN_POINT('',(2.1,1.175,0.04));
#22600=CARTESIAN_POINT('',(2.1,1.135,0.));
#22601=CARTESIAN_POINT('',(2.1,1.175,0.04));
#22602=CARTESIAN_POINT('Origin',(2.1,1.5,0.));
#22603=CARTESIAN_POINT('Origin',(2.1,1.5,0.04));
#22604=CARTESIAN_POINT('Origin',(2.05,1.155,0.02));
#22605=CARTESIAN_POINT('',(2.05,1.135,0.));
#22606=CARTESIAN_POINT('',(2.05,1.175,0.04));
#22607=CARTESIAN_POINT('Origin',(3.6,2.6,0.02));
#22608=CARTESIAN_POINT('',(3.6,2.96,0.));
#22609=CARTESIAN_POINT('',(3.6,2.96,0.));
#22610=CARTESIAN_POINT('Origin',(3.6,2.6,0.));
#22611=CARTESIAN_POINT('Origin',(2.,2.98,0.02));
#22612=CARTESIAN_POINT('',(-3.6,2.96,0.));
#22613=CARTESIAN_POINT('',(-3.6,2.96,0.));
#22614=CARTESIAN_POINT('',(2.,2.96,0.));
#22615=CARTESIAN_POINT('Origin',(-3.6,2.6,0.02));
#22616=CARTESIAN_POINT('Origin',(-3.6,2.6,0.));
#22617=CARTESIAN_POINT('Origin',(-2.1,1.5,0.8));
#22618=CARTESIAN_POINT('',(-2.1,1.175,0.74));
#22619=CARTESIAN_POINT('',(-2.1,1.175,0.8));
#22620=CARTESIAN_POINT('Origin',(-2.1,1.5,0.74));
#22621=CARTESIAN_POINT('Origin',(-2.1,1.175,0.8));
#22622=CARTESIAN_POINT('',(-1.05,1.175,0.74));
#22623=CARTESIAN_POINT('Origin',(-4.1,-1.175,0.8));
#22624=CARTESIAN_POINT('',(-2.1,-1.175,0.74));
#22625=CARTESIAN_POINT('',(-2.1,-1.175,0.8));
#22626=CARTESIAN_POINT('',(-2.05,-1.175,0.74));
#22627=CARTESIAN_POINT('Origin',(-2.1,-1.5,0.8));
#22628=CARTESIAN_POINT('',(-2.1,-1.825,0.74));
#22629=CARTESIAN_POINT('',(-2.1,-1.825,0.8));
#22630=CARTESIAN_POINT('Origin',(-2.1,-1.5,0.74));
#22631=CARTESIAN_POINT('Origin',(-2.1,-1.825,0.8));
#22632=CARTESIAN_POINT('',(-1.05,-1.825,0.74));
#22633=CARTESIAN_POINT('Origin',(0.,0.,0.));
#22634=CARTESIAN_POINT('Origin',(-3.6,-2.6,0.77));
#22635=CARTESIAN_POINT('',(-3.6,-3.,0.74));
#22636=CARTESIAN_POINT('Origin',(-3.6,-2.6,0.74));
#22637=CARTESIAN_POINT('',(-3.6,-3.,0.74));
#22638=CARTESIAN_POINT('Origin',(-2.,-2.97,0.77));
#22639=CARTESIAN_POINT('',(3.6,-3.,0.74));
#22640=CARTESIAN_POINT('',(-2.,-3.,0.74));
#22641=CARTESIAN_POINT('',(3.6,-3.,0.74));
#22642=CARTESIAN_POINT('Origin',(3.6,-2.6,0.77));
#22643=CARTESIAN_POINT('Origin',(3.6,-2.6,0.74));
#22644=CARTESIAN_POINT('Origin',(-2.05,-1.145,0.77));
#22645=CARTESIAN_POINT('',(-2.1,-1.175,0.74));
#22646=CARTESIAN_POINT('Origin',(-2.1,-1.5,0.77));
#22647=CARTESIAN_POINT('',(-2.1,-1.825,0.74));
#22648=CARTESIAN_POINT('Origin',(-1.05,-1.855,0.77));
#22649=CARTESIAN_POINT('Origin',(2.1,-1.5,0.77));
#22650=CARTESIAN_POINT('Origin',(2.1,-1.5,0.74));
#22651=CARTESIAN_POINT('Origin',(-2.1,1.5,0.77));
#22652=CARTESIAN_POINT('',(-2.1,1.175,0.74));
#22653=CARTESIAN_POINT('Origin',(-1.05,1.145,0.77));
#22654=CARTESIAN_POINT('Origin',(2.1,1.5,0.77));
#22655=CARTESIAN_POINT('Origin',(2.1,1.5,0.74));
#22656=CARTESIAN_POINT('Origin',(3.6,-2.6,0.));
#22657=CARTESIAN_POINT('',(3.6,-3.,0.));
#22658=CARTESIAN_POINT('Origin',(-4.,-3.,0.));
#22659=CARTESIAN_POINT('',(-3.6,-3.,0.));
#22660=CARTESIAN_POINT('Origin',(-3.6,-2.6,0.));
#22661=CARTESIAN_POINT('Origin',(4.1,1.175,0.8));
#22662=CARTESIAN_POINT('',(2.1,1.175,0.8));
#22663=CARTESIAN_POINT('Origin',(2.1,1.5,0.8));
#22664=CARTESIAN_POINT('Origin',(4.1,-1.825,0.8));
#22665=CARTESIAN_POINT('',(2.1,-1.825,0.8));
#22666=CARTESIAN_POINT('Origin',(2.1,-1.175,0.8));
#22667=CARTESIAN_POINT('',(2.1,-1.175,0.8));
#22668=CARTESIAN_POINT('Origin',(2.1,-1.5,0.8));
#38581=UNCERTAINTY_MEASURE_WITH_UNIT(LENGTH_MEASURE(0.001),#38612,
'DISTANCE_ACCURACY_VALUE',
'Maximum model space distance between geometric entities at asserted c
onnectivities');
#38595=UNCERTAINTY_MEASURE_WITH_UNIT(LENGTH_MEASURE(0.001),#38612,
'DISTANCE_ACCURACY_VALUE',
'Maximum model space distance between geometric entities at asserted c
onnectivities');
#38597=(
GEOMETRIC_REPRESENTATION_CONTEXT(3)
GLOBAL_UNCERTAINTY_ASSIGNED_CONTEXT((#38581))
GLOBAL_UNIT_ASSIGNED_CONTEXT((#38612,#38614,#38615))
REPRESENTATION_CONTEXT('','3D')
);
#38611=(
GEOMETRIC_REPRESENTATION_CONTEXT(3)
GLOBAL_UNCERTAINTY_ASSIGNED_CONTEXT((#38595))
GLOBAL_UNIT_ASSIGNED_CONTEXT((#38612,#38614,#38615))
REPRESENTATION_CONTEXT('','3D')
);
#38612=(
LENGTH_UNIT()
NAMED_UNIT(*)
SI_UNIT(.CENTI.,.METRE.)
);
#38614=(
NAMED_UNIT(*)
PLANE_ANGLE_UNIT()
SI_UNIT($,.RADIAN.)
);
#38615=(
NAMED_UNIT(*)
SI_UNIT($,.STERADIAN.)
SOLID_ANGLE_UNIT()
);
#38617=SHAPE_DEFINITION_REPRESENTATION(#38632,#38668);
#38632=PRODUCT_DEFINITION_SHAPE('',$,#38684);
#38668=SHAPE_REPRESENTATION('',(#16404),#38597);
#38682=PRODUCT_DEFINITION_CONTEXT('part definition',#38729,'design');
#38684=PRODUCT_DEFINITION('2026-10-19-02-31-24-157',
'01_Slotted_Foot_Base_with_Post_Socket_80x60',#38699,#38682);
#38699=PRODUCT_DEFINITION_FORMATION('',$,#38732);
#38729=APPLICATION_CONTEXT(
'Core Data for Automotive Mechanical Design Process');
#38730=PRODUCT_CONTEXT('part definition',#38729,'mechanical');
#38732=PRODUCT('2026-10-19-02-31-24-157',
'01_Slotted_Foot_Base_with_Post_Socket_80x60',$,(#38730));
#38851=COLOUR_RGB('Dark Blue',0.08,0.2,0.34);
#38852=FILL_AREA_STYLE_COLOUR('',#38851);
#38853=FILL_AREA_STYLE('',(#38852));
#38854=SURFACE_STYLE_FILL_AREA(#38853);
#38855=SURFACE_SIDE_STYLE('',(#38854));
#38856=SURFACE_STYLE_USAGE(.BOTH.,#38855);
#38857=PRESENTATION_STYLE_ASSIGNMENT((#38856));
ENDSEC;
END-ISO-10303-21;
